ISO-10303-21;
HEADER;
/* Generated by software containing ST-Developer
 * from STEP Tools, Inc. (www.steptools.com) 
 */
/* OPTION: using custom renumber hook */

FILE_DESCRIPTION(
/* description */ ('STEP AP242 Edition 2', 'CAx-IF Rec.Pracs.---Representation and Presentation of Product Manufa
cturing Information (PMI)---4.0---2014-10-13', 'CAx-IF Rec.Pracs.---3D Tessellated Geometry---0.4---2014-09-14', '2;1', 'CAx-IF Rec.Pracs.---User Defined Attributes---1.5---2016-08-15'),
/* implementation_level */ '2;1');

FILE_NAME(
/* name */ 'piston.step',
/* time_stamp */ '2026-10-08T12:15:07Z',
/* author */ (''),
/* organization */ (''),
/* preprocessor_version */ 'ST-DEVELOPER v20',
/* originating_system */ 'ONSHAPE BY PTC INC, 1.221',
/* authorisation */ '  ');

FILE_SCHEMA (('AP242_MANAGED_MODEL_BASED_3D_ENGINEERING_MIM_LF { 1 0 10303 442 3 1 4 }'));
ENDSEC;

DATA;
#21=CONICAL_SURFACE('',#13956,0.00075,0.436332312998577);
#40=B_SPLINE_SURFACE_WITH_KNOTS('',3,3,((#20040,#20041,#20042,#20043,#20044,
#20045,#20046,#20047,#20048,#20049,#20050,#20051,#20052,#20053,#20054,#20055,
#20056,#20057,#20058,#20059,#20060,#20061,#20062,#20063,#20064,#20065,#20066,
#20067,#20068,#20069,#20070,#20071,#20072,#20073,#20074,#20075,#20076,#20077,
#20078,#20079,#20080,#20081,#20082,#20083,#20084,#20085,#20086,#20087,#20088,
#20089,#20090,#20091,#20092,#20093,#20094,#20095),(#20096,#20097,#20098,
#20099,#20100,#20101,#20102,#20103,#20104,#20105,#20106,#20107,#20108,#20109,
#20110,#20111,#20112,#20113,#20114,#20115,#20116,#20117,#20118,#20119,#20120,
#20121,#20122,#20123,#20124,#20125,#20126,#20127,#20128,#20129,#20130,#20131,
#20132,#20133,#20134,#20135,#20136,#20137,#20138,#20139,#20140,#20141,#20142,
#20143,#20144,#20145,#20146,#20147,#20148,#20149,#20150,#20151),(#20152,
#20153,#20154,#20155,#20156,#20157,#20158,#20159,#20160,#20161,#20162,#20163,
#20164,#20165,#20166,#20167,#20168,#20169,#20170,#20171,#20172,#20173,#20174,
#20175,#20176,#20177,#20178,#20179,#20180,#20181,#20182,#20183,#20184,#20185,
#20186,#20187,#20188,#20189,#20190,#20191,#20192,#20193,#20194,#20195,#20196,
#20197,#20198,#20199,#20200,#20201,#20202,#20203,#20204,#20205,#20206,#20207),
(#20208,#20209,#20210,#20211,#20212,#20213,#20214,#20215,#20216,#20217,
#20218,#20219,#20220,#20221,#20222,#20223,#20224,#20225,#20226,#20227,#20228,
#20229,#20230,#20231,#20232,#20233,#20234,#20235,#20236,#20237,#20238,#20239,
#20240,#20241,#20242,#20243,#20244,#20245,#20246,#20247,#20248,#20249,#20250,
#20251,#20252,#20253,#20254,#20255,#20256,#20257,#20258,#20259,#20260,#20261,
#20262,#20263)),.UNSPECIFIED.,.F.,.F.,.F.,(4,4),(4,2,2,2,2,2,2,2,2,2,2,
2,2,2,2,2,2,2,2,2,2,2,2,2,2,2,2,4),(0.,1.),(0.,0.05198235199969,0.077973527999535,
0.10396470399938,0.129955879999225,0.15594705599907,0.181938231998915,0.20792940799876,
0.233920583998605,0.25991175999845,0.285902935998295,0.31189411199814,0.337885287997985,
0.36387646399783,0.389867639997675,0.41585881599752,0.441849991997365,0.46784116799721,
0.493832343997055,0.5198235199969,0.57180587199659,0.62378822399628,0.67577057599597,
0.72775292799566,0.77973527999535,0.805726455995195,0.818722043995117,0.83171763199504),
 .UNSPECIFIED.);
#60=COLOUR_RGB('', 0.66274510, 0.83137255, 0.94901961);
#202=SHAPE_REPRESENTATION_RELATIONSHIP('','',#13776,#229);
#229=ADVANCED_BREP_SHAPE_REPRESENTATION('',(#13720),#45466);
#256=TOROIDAL_SURFACE('',#13949,0.004,0.001);
#257=TOROIDAL_SURFACE('',#13961,0.0075,0.003);
#258=TOROIDAL_SURFACE('',#13969,0.0084,0.0001);
#259=TOROIDAL_SURFACE('',#13970,0.0084,0.0001);
#260=TOROIDAL_SURFACE('',#13971,0.0028,0.0002);
#261=TOROIDAL_SURFACE('',#13972,0.00095,0.0002);
#262=TOROIDAL_SURFACE('',#13973,0.0055,0.001);
#263=TOROIDAL_SURFACE('',#13974,0.0055,0.001);
#264=TOROIDAL_SURFACE('',#13975,0.0062,0.0003);
#265=TOROIDAL_SURFACE('',#13976,0.0062,0.0003);
#266=TOROIDAL_SURFACE('',#13977,0.0096,0.0003);
#267=TOROIDAL_SURFACE('',#13978,0.0096,0.0003);
#268=TOROIDAL_SURFACE('',#13979,0.008,0.0005);
#269=TOROIDAL_SURFACE('',#13983,0.0038,0.0003);
#270=TOROIDAL_SURFACE('',#13984,0.0038,0.0003);
#391=CIRCLE('',#13905,0.0045);
#392=CIRCLE('',#13906,0.0038);
#393=CIRCLE('',#13908,0.0045);
#394=CIRCLE('',#13909,0.0038);
#395=CIRCLE('',#13910,0.00651286233460729);
#396=CIRCLE('',#13913,0.0003);
#397=CIRCLE('',#13916,0.0084);
#398=CIRCLE('',#13917,0.0096);
#399=CIRCLE('',#13919,0.0084);
#400=CIRCLE('',#13920,0.0096);
#401=CIRCLE('',#13922,0.0075);
#402=CIRCLE('',#13923,0.0099);
#403=CIRCLE('',#13925,0.0055);
#404=CIRCLE('',#13926,0.0062);
#405=CIRCLE('',#13928,0.0055);
#406=CIRCLE('',#13929,0.0062);
#407=CIRCLE('',#13931,0.00261523063261997);
#408=CIRCLE('',#13932,0.0045);
#409=CIRCLE('',#13934,0.00095);
#410=CIRCLE('',#13935,0.0028);
#411=CIRCLE('',#13937,0.0075);
#412=CIRCLE('',#13938,0.004);
#413=CIRCLE('',#13940,0.0099);
#414=CIRCLE('',#13941,0.008);
#415=CIRCLE('',#13943,0.0045);
#416=CIRCLE('',#13945,0.0065);
#417=CIRCLE('',#13946,0.0065);
#418=CIRCLE('',#13948,0.0075);
#419=CIRCLE('',#13950,0.003);
#420=CIRCLE('',#13952,0.003);
#421=CIRCLE('',#13954,0.00075);
#422=CIRCLE('',#13955,0.00075);
#423=CIRCLE('',#13959,0.0045);
#424=CIRCLE('',#13960,0.0045);
#425=CIRCLE('',#13963,0.0099);
#426=CIRCLE('',#13965,0.0083);
#427=CIRCLE('',#13966,0.0083);
#428=CIRCLE('',#13968,0.0099);
#429=CIRCLE('',#13981,0.0035);
#430=CIRCLE('',#13982,0.0035);
#1065=B_SPLINE_CURVE_WITH_KNOTS('',3,(#19997,#19998,#19999,#20000,#20001),
 .UNSPECIFIED.,.F.,.F.,(4,1,4),(4.46872309623959E-16,0.00181535454777857,
0.0036307090955567),.UNSPECIFIED.);
#1220=PLANE('',#13904);
#1221=PLANE('',#13907);
#1222=PLANE('',#13912);
#1223=PLANE('',#13914);
#1224=PLANE('',#13915);
#1225=PLANE('',#13918);
#1226=PLANE('',#13921);
#1227=PLANE('',#13924);
#1228=PLANE('',#13927);
#1229=PLANE('',#13930);
#1230=PLANE('',#13933);
#1231=PLANE('',#13936);
#1232=PLANE('',#13939);
#1564=CYLINDRICAL_SURFACE('',#13911,0.00748201094464285);
#1565=CYLINDRICAL_SURFACE('',#13942,0.0045);
#1566=CYLINDRICAL_SURFACE('',#13944,0.0065);
#1567=CYLINDRICAL_SURFACE('',#13947,0.0075);
#1568=CYLINDRICAL_SURFACE('',#13951,0.003);
#1569=CYLINDRICAL_SURFACE('',#13953,0.00075);
#1570=CYLINDRICAL_SURFACE('',#13957,0.0045);
#1571=CYLINDRICAL_SURFACE('',#13958,0.0045);
#1572=CYLINDRICAL_SURFACE('',#13962,0.0099);
#1573=CYLINDRICAL_SURFACE('',#13964,0.0083);
#1574=CYLINDRICAL_SURFACE('',#13967,0.0099);
#1575=CYLINDRICAL_SURFACE('',#13980,0.0035);
#1842=(
BOUNDED_CURVE()
B_SPLINE_CURVE(2,(#19957,#19958,#19959,#19960,#19961,#19962,#19963,#19964,
#19965,#19966,#19967,#19968,#19969,#19970,#19971,#19972,#19973,#19974,#19975,
#19976,#19977,#19978,#19979,#19980,#19981,#19982,#19983,#19984,#19985,#19986,
#19987,#19988,#19989,#19990,#19991),.UNSPECIFIED.,.F.,.F.)
B_SPLINE_CURVE_WITH_KNOTS((3,2,2,2,2,2,2,2,2,2,2,2,2,2,2,2,2,3),(0.,0.05,
0.1,0.15,0.2,0.25,0.3,0.35,0.4,0.45,0.5,0.55,0.6,0.65,0.7,0.75,0.8,0.826757086852849),
 .UNSPECIFIED.)
CURVE()
GEOMETRIC_REPRESENTATION_ITEM()
RATIONAL_B_SPLINE_CURVE((1.,0.951056516295154,1.,0.951056516295154,1.,0.951056516295154,
1.,0.951056516295154,1.,0.951056516295154,1.,0.951056516295154,1.,0.951056516295154,
1.,0.951056516295154,1.,0.951056516295154,1.,0.951056516295154,1.,0.951056516295154,
1.,0.951056516295154,1.,0.951056516295154,1.,0.951056516295154,1.,0.951056516295154,
1.,0.951056516295154,1.,0.973808299112568,0.975649142843891))
REPRESENTATION_ITEM('')
);
#1843=(
BOUNDED_CURVE()
B_SPLINE_CURVE(2,(#20005,#20006,#20007,#20008,#20009,#20010,#20011,#20012,
#20013,#20014,#20015),.UNSPECIFIED.,.F.,.F.)
B_SPLINE_CURVE_WITH_KNOTS((3,2,2,2,2,3),(0.5,0.55,0.6,0.65,0.7,0.75),
 .UNSPECIFIED.)
CURVE()
GEOMETRIC_REPRESENTATION_ITEM()
RATIONAL_B_SPLINE_CURVE((1.,0.951056516295153,1.,0.951056516295154,1.,0.951056516295154,
1.,0.951056516295154,1.,0.951056516295155,1.))
REPRESENTATION_ITEM('')
);
#1844=(
BOUNDED_CURVE()
B_SPLINE_CURVE(2,(#20017,#20018,#20019,#20020,#20021,#20022,#20023,#20024,
#20025,#20026,#20027),.UNSPECIFIED.,.F.,.F.)
B_SPLINE_CURVE_WITH_KNOTS((3,2,2,2,2,3),(0.25,0.3,0.35,0.4,0.45,0.5),
 .UNSPECIFIED.)
CURVE()
GEOMETRIC_REPRESENTATION_ITEM()
RATIONAL_B_SPLINE_CURVE((1.,0.951056516295153,1.,0.951056516295154,1.,0.951056516295154,
1.,0.951056516295154,1.,0.951056516295154,1.))
REPRESENTATION_ITEM('')
);
#1845=(
BOUNDED_CURVE()
B_SPLINE_CURVE(2,(#20029,#20030,#20031,#20032,#20033,#20034,#20035,#20036,
#20037,#20038,#20039),.UNSPECIFIED.,.F.,.F.)
B_SPLINE_CURVE_WITH_KNOTS((3,2,2,2,2,3),(0.,0.05,0.1,0.15,0.2,0.25),
 .UNSPECIFIED.)
CURVE()
GEOMETRIC_REPRESENTATION_ITEM()
RATIONAL_B_SPLINE_CURVE((1.,0.951056516295154,1.,0.951056516295154,1.,0.951056516295154,
1.,0.951056516295154,1.,0.951056516295154,1.))
REPRESENTATION_ITEM('')
);
#1846=(
BOUNDED_CURVE()
B_SPLINE_CURVE(2,(#20267,#20268,#20269,#20270,#20271,#20272,#20273,#20274,
#20275,#20276,#20277),.UNSPECIFIED.,.F.,.F.)
B_SPLINE_CURVE_WITH_KNOTS((3,2,2,2,2,3),(0.,0.05,0.1,0.15,0.2,0.25),
 .UNSPECIFIED.)
CURVE()
GEOMETRIC_REPRESENTATION_ITEM()
RATIONAL_B_SPLINE_CURVE((1.,0.951056516295154,1.,0.951056516295154,1.,0.951056516295154,
1.,0.951056516295154,1.,0.951056516295154,1.))
REPRESENTATION_ITEM('')
);
#1847=(
BOUNDED_CURVE()
B_SPLINE_CURVE(2,(#20279,#20280,#20281,#20282,#20283,#20284,#20285,#20286,
#20287,#20288,#20289),.UNSPECIFIED.,.F.,.F.)
B_SPLINE_CURVE_WITH_KNOTS((3,2,2,2,2,3),(0.25,0.3,0.35,0.4,0.45,0.5),
 .UNSPECIFIED.)
CURVE()
GEOMETRIC_REPRESENTATION_ITEM()
RATIONAL_B_SPLINE_CURVE((1.,0.951056516295153,1.,0.951056516295154,1.,0.951056516295154,
1.,0.951056516295154,1.,0.951056516295154,1.))
REPRESENTATION_ITEM('')
);
#1848=(
BOUNDED_CURVE()
B_SPLINE_CURVE(2,(#20291,#20292,#20293,#20294,#20295,#20296,#20297,#20298,
#20299,#20300,#20301),.UNSPECIFIED.,.F.,.F.)
B_SPLINE_CURVE_WITH_KNOTS((3,2,2,2,2,3),(0.5,0.55,0.6,0.65,0.7,0.75),
 .UNSPECIFIED.)
CURVE()
GEOMETRIC_REPRESENTATION_ITEM()
RATIONAL_B_SPLINE_CURVE((1.,0.951056516295153,1.,0.951056516295154,1.,0.951056516295154,
1.,0.951056516295154,1.,0.951056516295155,1.))
REPRESENTATION_ITEM('')
);
#1849=(
BOUNDED_CURVE()
B_SPLINE_CURVE(2,(#20303,#20304,#20305,#20306,#20307),.UNSPECIFIED.,.F.,
 .F.)
B_SPLINE_CURVE_WITH_KNOTS((3,2,3),(0.75,0.8,0.826757130829527),
 .UNSPECIFIED.)
CURVE()
GEOMETRIC_REPRESENTATION_ITEM()
RATIONAL_B_SPLINE_CURVE((1.,0.951056516295153,1.,0.973808256065132,0.975649148895013))
REPRESENTATION_ITEM('')
);
#1850=(
BOUNDED_CURVE()
B_SPLINE_CURVE(2,(#20311,#20312,#20313,#20314,#20315,#20316,#20317,#20318,
#20319,#20320,#20321,#20322,#20323,#20324,#20325,#20326,#20327,#20328,#20329,
#20330,#20331,#20332,#20333,#20334,#20335,#20336,#20337,#20338,#20339,#20340,
#20341,#20342,#20343,#20344,#20345),.UNSPECIFIED.,.F.,.F.)
B_SPLINE_CURVE_WITH_KNOTS((3,2,2,2,2,2,2,2,2,2,2,2,2,2,2,2,2,3),(0.,0.05,
0.1,0.15,0.2,0.25,0.3,0.35,0.4,0.45,0.5,0.55,0.6,0.65,0.7,0.75,0.8,0.826757072590209),
 .UNSPECIFIED.)
CURVE()
GEOMETRIC_REPRESENTATION_ITEM()
RATIONAL_B_SPLINE_CURVE((1.,0.951056516295154,1.,0.951056516295154,1.,0.951056516295154,
1.,0.951056516295154,1.,0.951056516295154,1.,0.951056516295154,1.,0.951056516295154,
1.,0.951056516295154,1.,0.951056516295154,1.,0.951056516295154,1.,0.951056516295154,
1.,0.951056516295154,1.,0.951056516295154,1.,0.951056516295154,1.,0.951056516295154,
1.,0.951056516295154,1.,0.973808313073834,0.975649140881406))
REPRESENTATION_ITEM('')
);
#2178=ORIENTED_EDGE('',*,*,#5736,.F.);
#2179=ORIENTED_EDGE('',*,*,#5737,.T.);
#2180=ORIENTED_EDGE('',*,*,#5738,.F.);
#2181=ORIENTED_EDGE('',*,*,#5739,.T.);
#2182=ORIENTED_EDGE('',*,*,#5740,.F.);
#2183=ORIENTED_EDGE('',*,*,#5741,.T.);
#2184=ORIENTED_EDGE('',*,*,#5742,.F.);
#2185=ORIENTED_EDGE('',*,*,#5743,.T.);
#2186=ORIENTED_EDGE('',*,*,#5744,.T.);
#2187=ORIENTED_EDGE('',*,*,#5745,.F.);
#2188=ORIENTED_EDGE('',*,*,#5746,.F.);
#2189=ORIENTED_EDGE('',*,*,#5747,.F.);
#2190=ORIENTED_EDGE('',*,*,#5748,.F.);
#2191=ORIENTED_EDGE('',*,*,#5749,.F.);
#2192=ORIENTED_EDGE('',*,*,#5750,.T.);
#2193=ORIENTED_EDGE('',*,*,#5751,.T.);
#2194=ORIENTED_EDGE('',*,*,#5752,.T.);
#2195=ORIENTED_EDGE('',*,*,#5753,.T.);
#2196=ORIENTED_EDGE('',*,*,#5754,.F.);
#2197=ORIENTED_EDGE('',*,*,#5755,.F.);
#2198=ORIENTED_EDGE('',*,*,#5756,.F.);
#2199=ORIENTED_EDGE('',*,*,#5755,.T.);
#2200=ORIENTED_EDGE('',*,*,#5757,.F.);
#2201=ORIENTED_EDGE('',*,*,#5741,.F.);
#2202=ORIENTED_EDGE('',*,*,#5757,.T.);
#2203=ORIENTED_EDGE('',*,*,#5754,.T.);
#2204=ORIENTED_EDGE('',*,*,#5758,.T.);
#2205=ORIENTED_EDGE('',*,*,#5759,.T.);
#2206=ORIENTED_EDGE('',*,*,#5743,.F.);
#2207=ORIENTED_EDGE('',*,*,#5742,.T.);
#2208=ORIENTED_EDGE('',*,*,#5756,.T.);
#2209=ORIENTED_EDGE('',*,*,#5740,.T.);
#2210=ORIENTED_EDGE('',*,*,#5760,.T.);
#2211=ORIENTED_EDGE('',*,*,#5749,.T.);
#2212=ORIENTED_EDGE('',*,*,#5761,.T.);
#2213=ORIENTED_EDGE('',*,*,#5762,.T.);
#2214=ORIENTED_EDGE('',*,*,#5763,.T.);
#2215=ORIENTED_EDGE('',*,*,#5764,.T.);
#2216=ORIENTED_EDGE('',*,*,#5765,.T.);
#2217=ORIENTED_EDGE('',*,*,#5766,.F.);
#2218=ORIENTED_EDGE('',*,*,#5767,.T.);
#2219=ORIENTED_EDGE('',*,*,#5768,.T.);
#2220=ORIENTED_EDGE('',*,*,#5769,.T.);
#2221=ORIENTED_EDGE('',*,*,#5770,.T.);
#2222=ORIENTED_EDGE('',*,*,#5771,.T.);
#2223=ORIENTED_EDGE('',*,*,#5772,.F.);
#2224=ORIENTED_EDGE('',*,*,#5773,.T.);
#2225=ORIENTED_EDGE('',*,*,#5774,.T.);
#2226=ORIENTED_EDGE('',*,*,#5775,.T.);
#2227=ORIENTED_EDGE('',*,*,#5776,.F.);
#2228=ORIENTED_EDGE('',*,*,#5777,.T.);
#2229=ORIENTED_EDGE('',*,*,#5778,.T.);
#2230=ORIENTED_EDGE('',*,*,#5779,.T.);
#2231=ORIENTED_EDGE('',*,*,#5738,.T.);
#2232=ORIENTED_EDGE('',*,*,#5746,.T.);
#2233=ORIENTED_EDGE('',*,*,#5745,.T.);
#2234=ORIENTED_EDGE('',*,*,#5780,.T.);
#2235=ORIENTED_EDGE('',*,*,#5758,.F.);
#2236=ORIENTED_EDGE('',*,*,#5753,.F.);
#2237=ORIENTED_EDGE('',*,*,#5752,.F.);
#2238=ORIENTED_EDGE('',*,*,#5751,.F.);
#2239=ORIENTED_EDGE('',*,*,#5750,.F.);
#2240=ORIENTED_EDGE('',*,*,#5760,.F.);
#2241=ORIENTED_EDGE('',*,*,#5748,.T.);
#2242=ORIENTED_EDGE('',*,*,#5747,.T.);
#2243=ORIENTED_EDGE('',*,*,#5781,.T.);
#2244=ORIENTED_EDGE('',*,*,#5782,.T.);
#2245=ORIENTED_EDGE('',*,*,#5775,.F.);
#2246=ORIENTED_EDGE('',*,*,#5783,.F.);
#2247=ORIENTED_EDGE('',*,*,#5776,.T.);
#2248=ORIENTED_EDGE('',*,*,#5783,.T.);
#2249=ORIENTED_EDGE('',*,*,#5784,.T.);
#2250=ORIENTED_EDGE('',*,*,#5785,.T.);
#2251=ORIENTED_EDGE('',*,*,#5786,.F.);
#2252=ORIENTED_EDGE('',*,*,#5771,.F.);
#2253=ORIENTED_EDGE('',*,*,#5786,.T.);
#2254=ORIENTED_EDGE('',*,*,#5736,.T.);
#2255=ORIENTED_EDGE('',*,*,#5772,.T.);
#2256=ORIENTED_EDGE('',*,*,#5787,.F.);
#2257=ORIENTED_EDGE('',*,*,#5788,.T.);
#2258=ORIENTED_EDGE('',*,*,#5787,.T.);
#2259=ORIENTED_EDGE('',*,*,#5765,.F.);
#2260=ORIENTED_EDGE('',*,*,#5789,.T.);
#2261=ORIENTED_EDGE('',*,*,#5766,.T.);
#2262=ORIENTED_EDGE('',*,*,#5790,.T.);
#2263=ORIENTED_EDGE('',*,*,#5791,.T.);
#2264=ORIENTED_EDGE('',*,*,#5777,.F.);
#2265=ORIENTED_EDGE('',*,*,#5792,.T.);
#2266=ORIENTED_EDGE('',*,*,#5791,.F.);
#2267=ORIENTED_EDGE('',*,*,#5763,.F.);
#2268=ORIENTED_EDGE('',*,*,#5790,.F.);
#2269=ORIENTED_EDGE('',*,*,#5761,.F.);
#2270=ORIENTED_EDGE('',*,*,#5774,.F.);
#2271=ORIENTED_EDGE('',*,*,#5784,.F.);
#2272=ORIENTED_EDGE('',*,*,#5773,.F.);
#2273=ORIENTED_EDGE('',*,*,#5785,.F.);
#2274=ORIENTED_EDGE('',*,*,#5788,.F.);
#2275=ORIENTED_EDGE('',*,*,#5767,.F.);
#2276=ORIENTED_EDGE('',*,*,#5779,.F.);
#2277=ORIENTED_EDGE('',*,*,#5769,.F.);
#2278=ORIENTED_EDGE('',*,*,#5780,.F.);
#2279=ORIENTED_EDGE('',*,*,#5744,.F.);
#2280=ORIENTED_EDGE('',*,*,#5759,.F.);
#2281=ORIENTED_EDGE('',*,*,#5768,.F.);
#2282=ORIENTED_EDGE('',*,*,#5781,.F.);
#2283=ORIENTED_EDGE('',*,*,#5770,.F.);
#2284=ORIENTED_EDGE('',*,*,#5792,.F.);
#2285=ORIENTED_EDGE('',*,*,#5762,.F.);
#2286=ORIENTED_EDGE('',*,*,#5789,.F.);
#2287=ORIENTED_EDGE('',*,*,#5764,.F.);
#2288=ORIENTED_EDGE('',*,*,#5778,.F.);
#2289=ORIENTED_EDGE('',*,*,#5782,.F.);
#2290=ORIENTED_EDGE('',*,*,#5793,.T.);
#2291=ORIENTED_EDGE('',*,*,#5794,.T.);
#2292=ORIENTED_EDGE('',*,*,#5794,.F.);
#2293=ORIENTED_EDGE('',*,*,#5739,.F.);
#2294=ORIENTED_EDGE('',*,*,#5793,.F.);
#2295=ORIENTED_EDGE('',*,*,#5737,.F.);
#5736=EDGE_CURVE('',#7549,#7549,#391,.T.);
#5737=EDGE_CURVE('',#7550,#7550,#392,.T.);
#5738=EDGE_CURVE('',#7551,#7551,#393,.T.);
#5739=EDGE_CURVE('',#7552,#7552,#394,.T.);
#5740=EDGE_CURVE('',#7553,#7554,#8806,.T.);
#5741=EDGE_CURVE('',#7553,#7555,#1842,.T.);
#5742=EDGE_CURVE('',#7556,#7555,#8807,.T.);
#5743=EDGE_CURVE('',#7556,#7557,#8808,.T.);
#5744=EDGE_CURVE('',#7557,#7558,#1065,.T.);
#5745=EDGE_CURVE('',#7559,#7558,#395,.T.);
#5746=EDGE_CURVE('',#7560,#7559,#1843,.T.);
#5747=EDGE_CURVE('',#7561,#7560,#1844,.T.);
#5748=EDGE_CURVE('',#7554,#7561,#1845,.T.);
#5749=EDGE_CURVE('',#7562,#7563,#8809,.T.);
#5750=EDGE_CURVE('',#7562,#7564,#1846,.T.);
#5751=EDGE_CURVE('',#7564,#7565,#1847,.T.);
#5752=EDGE_CURVE('',#7565,#7566,#1848,.T.);
#5753=EDGE_CURVE('',#7566,#7567,#1849,.T.);
#5754=EDGE_CURVE('',#7568,#7567,#8810,.T.);
#5755=EDGE_CURVE('',#7563,#7568,#1850,.T.);
#5756=EDGE_CURVE('',#7563,#7553,#8811,.T.);
#5757=EDGE_CURVE('',#7555,#7568,#8812,.T.);
#5758=EDGE_CURVE('',#7567,#7569,#8813,.T.);
#5759=EDGE_CURVE('',#7569,#7557,#396,.T.);
#5760=EDGE_CURVE('',#7554,#7562,#8814,.T.);
#5761=EDGE_CURVE('',#7570,#7570,#397,.T.);
#5762=EDGE_CURVE('',#7571,#7571,#398,.T.);
#5763=EDGE_CURVE('',#7572,#7572,#399,.T.);
#5764=EDGE_CURVE('',#7573,#7573,#400,.T.);
#5765=EDGE_CURVE('',#7574,#7574,#401,.T.);
#5766=EDGE_CURVE('',#7575,#7575,#402,.T.);
#5767=EDGE_CURVE('',#7576,#7576,#403,.T.);
#5768=EDGE_CURVE('',#7577,#7577,#404,.T.);
#5769=EDGE_CURVE('',#7578,#7578,#405,.T.);
#5770=EDGE_CURVE('',#7579,#7579,#406,.T.);
#5771=EDGE_CURVE('',#7580,#7580,#407,.T.);
#5772=EDGE_CURVE('',#7581,#7581,#408,.T.);
#5773=EDGE_CURVE('',#7582,#7582,#409,.T.);
#5774=EDGE_CURVE('',#7583,#7583,#410,.T.);
#5775=EDGE_CURVE('',#7584,#7584,#411,.T.);
#5776=EDGE_CURVE('',#7585,#7585,#412,.T.);
#5777=EDGE_CURVE('',#7586,#7586,#413,.T.);
#5778=EDGE_CURVE('',#7587,#7587,#414,.T.);
#5779=EDGE_CURVE('',#7588,#7588,#415,.T.);
#5780=EDGE_CURVE('',#7558,#7569,#416,.T.);
#5781=EDGE_CURVE('',#7589,#7589,#417,.T.);
#5782=EDGE_CURVE('',#7590,#7590,#418,.T.);
#5783=EDGE_CURVE('',#7591,#7591,#419,.T.);
#5784=EDGE_CURVE('',#7592,#7592,#420,.T.);
#5785=EDGE_CURVE('',#7593,#7593,#421,.T.);
#5786=EDGE_CURVE('',#7594,#7594,#422,.T.);
#5787=EDGE_CURVE('',#7595,#7595,#423,.T.);
#5788=EDGE_CURVE('',#7596,#7596,#424,.T.);
#5789=EDGE_CURVE('',#7597,#7597,#425,.T.);
#5790=EDGE_CURVE('',#7598,#7598,#426,.T.);
#5791=EDGE_CURVE('',#7599,#7599,#427,.T.);
#5792=EDGE_CURVE('',#7600,#7600,#428,.T.);
#5793=EDGE_CURVE('',#7601,#7601,#429,.T.);
#5794=EDGE_CURVE('',#7602,#7602,#430,.T.);
#7549=VERTEX_POINT('',#19841);
#7550=VERTEX_POINT('',#19843);
#7551=VERTEX_POINT('',#19846);
#7552=VERTEX_POINT('',#19848);
#7553=VERTEX_POINT('',#19955);
#7554=VERTEX_POINT('',#19956);
#7555=VERTEX_POINT('',#19992);
#7556=VERTEX_POINT('',#19994);
#7557=VERTEX_POINT('',#19996);
#7558=VERTEX_POINT('',#20002);
#7559=VERTEX_POINT('',#20004);
#7560=VERTEX_POINT('',#20016);
#7561=VERTEX_POINT('',#20028);
#7562=VERTEX_POINT('',#20265);
#7563=VERTEX_POINT('',#20266);
#7564=VERTEX_POINT('',#20278);
#7565=VERTEX_POINT('',#20290);
#7566=VERTEX_POINT('',#20302);
#7567=VERTEX_POINT('',#20308);
#7568=VERTEX_POINT('',#20310);
#7569=VERTEX_POINT('',#20351);
#7570=VERTEX_POINT('',#20357);
#7571=VERTEX_POINT('',#20359);
#7572=VERTEX_POINT('',#20362);
#7573=VERTEX_POINT('',#20364);
#7574=VERTEX_POINT('',#20367);
#7575=VERTEX_POINT('',#20369);
#7576=VERTEX_POINT('',#20372);
#7577=VERTEX_POINT('',#20374);
#7578=VERTEX_POINT('',#20377);
#7579=VERTEX_POINT('',#20379);
#7580=VERTEX_POINT('',#20382);
#7581=VERTEX_POINT('',#20384);
#7582=VERTEX_POINT('',#20387);
#7583=VERTEX_POINT('',#20389);
#7584=VERTEX_POINT('',#20392);
#7585=VERTEX_POINT('',#20394);
#7586=VERTEX_POINT('',#20397);
#7587=VERTEX_POINT('',#20399);
#7588=VERTEX_POINT('',#20402);
#7589=VERTEX_POINT('',#20406);
#7590=VERTEX_POINT('',#20409);
#7591=VERTEX_POINT('',#20412);
#7592=VERTEX_POINT('',#20415);
#7593=VERTEX_POINT('',#20418);
#7594=VERTEX_POINT('',#20420);
#7595=VERTEX_POINT('',#20425);
#7596=VERTEX_POINT('',#20427);
#7597=VERTEX_POINT('',#20431);
#7598=VERTEX_POINT('',#20434);
#7599=VERTEX_POINT('',#20436);
#7600=VERTEX_POINT('',#20439);
#7601=VERTEX_POINT('',#20453);
#7602=VERTEX_POINT('',#20455);
#8806=LINE('',#19954,#9634);
#8807=LINE('',#19993,#9635);
#8808=LINE('',#19995,#9636);
#8809=LINE('',#20264,#9637);
#8810=LINE('',#20309,#9638);
#8811=LINE('',#20347,#9639);
#8812=LINE('',#20348,#9640);
#8813=LINE('',#20350,#9641);
#8814=LINE('',#20354,#9642);
#9634=VECTOR('',#15544,1.);
#9635=VECTOR('',#15545,1.);
#9636=VECTOR('',#15546,1.);
#9637=VECTOR('',#15549,1.);
#9638=VECTOR('',#15550,1.);
#9639=VECTOR('',#15553,1.);
#9640=VECTOR('',#15554,1.);
#9641=VECTOR('',#15557,1.);
#9642=VECTOR('',#15562,1.);
#10532=EDGE_LOOP('',(#2178));
#10533=EDGE_LOOP('',(#2179));
#10534=EDGE_LOOP('',(#2180));
#10535=EDGE_LOOP('',(#2181));
#10536=EDGE_LOOP('',(#2182,#2183,#2184,#2185,#2186,#2187,#2188,#2189,#2190));
#10537=EDGE_LOOP('',(#2191,#2192,#2193,#2194,#2195,#2196,#2197));
#10538=EDGE_LOOP('',(#2198,#2199,#2200,#2201));
#10539=EDGE_LOOP('',(#2202,#2203,#2204,#2205,#2206,#2207));
#10540=EDGE_LOOP('',(#2208,#2209,#2210,#2211));
#10541=EDGE_LOOP('',(#2212));
#10542=EDGE_LOOP('',(#2213));
#10543=EDGE_LOOP('',(#2214));
#10544=EDGE_LOOP('',(#2215));
#10545=EDGE_LOOP('',(#2216));
#10546=EDGE_LOOP('',(#2217));
#10547=EDGE_LOOP('',(#2218));
#10548=EDGE_LOOP('',(#2219));
#10549=EDGE_LOOP('',(#2220));
#10550=EDGE_LOOP('',(#2221));
#10551=EDGE_LOOP('',(#2222));
#10552=EDGE_LOOP('',(#2223));
#10553=EDGE_LOOP('',(#2224));
#10554=EDGE_LOOP('',(#2225));
#10555=EDGE_LOOP('',(#2226));
#10556=EDGE_LOOP('',(#2227));
#10557=EDGE_LOOP('',(#2228));
#10558=EDGE_LOOP('',(#2229));
#10559=EDGE_LOOP('',(#2230));
#10560=EDGE_LOOP('',(#2231));
#10561=EDGE_LOOP('',(#2232,#2233,#2234,#2235,#2236,#2237,#2238,#2239,#2240,
#2241,#2242));
#10562=EDGE_LOOP('',(#2243));
#10563=EDGE_LOOP('',(#2244));
#10564=EDGE_LOOP('',(#2245));
#10565=EDGE_LOOP('',(#2246));
#10566=EDGE_LOOP('',(#2247));
#10567=EDGE_LOOP('',(#2248));
#10568=EDGE_LOOP('',(#2249));
#10569=EDGE_LOOP('',(#2250));
#10570=EDGE_LOOP('',(#2251));
#10571=EDGE_LOOP('',(#2252));
#10572=EDGE_LOOP('',(#2253));
#10573=EDGE_LOOP('',(#2254));
#10574=EDGE_LOOP('',(#2255));
#10575=EDGE_LOOP('',(#2256));
#10576=EDGE_LOOP('',(#2257));
#10577=EDGE_LOOP('',(#2258));
#10578=EDGE_LOOP('',(#2259));
#10579=EDGE_LOOP('',(#2260));
#10580=EDGE_LOOP('',(#2261));
#10581=EDGE_LOOP('',(#2262));
#10582=EDGE_LOOP('',(#2263));
#10583=EDGE_LOOP('',(#2264));
#10584=EDGE_LOOP('',(#2265));
#10585=EDGE_LOOP('',(#2266));
#10586=EDGE_LOOP('',(#2267));
#10587=EDGE_LOOP('',(#2268));
#10588=EDGE_LOOP('',(#2269));
#10589=EDGE_LOOP('',(#2270));
#10590=EDGE_LOOP('',(#2271));
#10591=EDGE_LOOP('',(#2272));
#10592=EDGE_LOOP('',(#2273));
#10593=EDGE_LOOP('',(#2274));
#10594=EDGE_LOOP('',(#2275));
#10595=EDGE_LOOP('',(#2276));
#10596=EDGE_LOOP('',(#2277));
#10597=EDGE_LOOP('',(#2278,#2279,#2280));
#10598=EDGE_LOOP('',(#2281));
#10599=EDGE_LOOP('',(#2282));
#10600=EDGE_LOOP('',(#2283));
#10601=EDGE_LOOP('',(#2284));
#10602=EDGE_LOOP('',(#2285));
#10603=EDGE_LOOP('',(#2286));
#10604=EDGE_LOOP('',(#2287));
#10605=EDGE_LOOP('',(#2288));
#10606=EDGE_LOOP('',(#2289));
#10607=EDGE_LOOP('',(#2290));
#10608=EDGE_LOOP('',(#2291));
#10609=EDGE_LOOP('',(#2292));
#10610=EDGE_LOOP('',(#2293));
#10611=EDGE_LOOP('',(#2294));
#10612=EDGE_LOOP('',(#2295));
#11647=FACE_BOUND('',#10532,.T.);
#11648=FACE_BOUND('',#10533,.T.);
#11649=FACE_BOUND('',#10534,.T.);
#11650=FACE_BOUND('',#10535,.T.);
#11651=FACE_BOUND('',#10536,.T.);
#11652=FACE_BOUND('',#10537,.T.);
#11653=FACE_BOUND('',#10538,.T.);
#11654=FACE_BOUND('',#10539,.T.);
#11655=FACE_BOUND('',#10540,.T.);
#11656=FACE_BOUND('',#10541,.T.);
#11657=FACE_BOUND('',#10542,.T.);
#11658=FACE_BOUND('',#10543,.T.);
#11659=FACE_BOUND('',#10544,.T.);
#11660=FACE_BOUND('',#10545,.T.);
#11661=FACE_BOUND('',#10546,.T.);
#11662=FACE_BOUND('',#10547,.T.);
#11663=FACE_BOUND('',#10548,.T.);
#11664=FACE_BOUND('',#10549,.T.);
#11665=FACE_BOUND('',#10550,.T.);
#11666=FACE_BOUND('',#10551,.T.);
#11667=FACE_BOUND('',#10552,.T.);
#11668=FACE_BOUND('',#10553,.T.);
#11669=FACE_BOUND('',#10554,.T.);
#11670=FACE_BOUND('',#10555,.T.);
#11671=FACE_BOUND('',#10556,.T.);
#11672=FACE_BOUND('',#10557,.T.);
#11673=FACE_BOUND('',#10558,.T.);
#11674=FACE_BOUND('',#10559,.T.);
#11675=FACE_BOUND('',#10560,.T.);
#11676=FACE_BOUND('',#10561,.T.);
#11677=FACE_BOUND('',#10562,.T.);
#11678=FACE_BOUND('',#10563,.T.);
#11679=FACE_BOUND('',#10564,.T.);
#11680=FACE_BOUND('',#10565,.T.);
#11681=FACE_BOUND('',#10566,.T.);
#11682=FACE_BOUND('',#10567,.T.);
#11683=FACE_BOUND('',#10568,.T.);
#11684=FACE_BOUND('',#10569,.T.);
#11685=FACE_BOUND('',#10570,.T.);
#11686=FACE_BOUND('',#10571,.T.);
#11687=FACE_BOUND('',#10572,.T.);
#11688=FACE_BOUND('',#10573,.T.);
#11689=FACE_BOUND('',#10574,.T.);
#11690=FACE_BOUND('',#10575,.T.);
#11691=FACE_BOUND('',#10576,.T.);
#11692=FACE_BOUND('',#10577,.T.);
#11693=FACE_BOUND('',#10578,.T.);
#11694=FACE_BOUND('',#10579,.T.);
#11695=FACE_BOUND('',#10580,.T.);
#11696=FACE_BOUND('',#10581,.T.);
#11697=FACE_BOUND('',#10582,.T.);
#11698=FACE_BOUND('',#10583,.T.);
#11699=FACE_BOUND('',#10584,.T.);
#11700=FACE_BOUND('',#10585,.T.);
#11701=FACE_BOUND('',#10586,.T.);
#11702=FACE_BOUND('',#10587,.T.);
#11703=FACE_BOUND('',#10588,.T.);
#11704=FACE_BOUND('',#10589,.T.);
#11705=FACE_BOUND('',#10590,.T.);
#11706=FACE_BOUND('',#10591,.T.);
#11707=FACE_BOUND('',#10592,.T.);
#11708=FACE_BOUND('',#10593,.T.);
#11709=FACE_BOUND('',#10594,.T.);
#11710=FACE_BOUND('',#10595,.T.);
#11711=FACE_BOUND('',#10596,.T.);
#11712=FACE_BOUND('',#10597,.T.);
#11713=FACE_BOUND('',#10598,.T.);
#11714=FACE_BOUND('',#10599,.T.);
#11715=FACE_BOUND('',#10600,.T.);
#11716=FACE_BOUND('',#10601,.T.);
#11717=FACE_BOUND('',#10602,.T.);
#11718=FACE_BOUND('',#10603,.T.);
#11719=FACE_BOUND('',#10604,.T.);
#11720=FACE_BOUND('',#10605,.T.);
#11721=FACE_BOUND('',#10606,.T.);
#11722=FACE_BOUND('',#10607,.T.);
#11723=FACE_BOUND('',#10608,.T.);
#11724=FACE_BOUND('',#10609,.T.);
#11725=FACE_BOUND('',#10610,.T.);
#11726=FACE_BOUND('',#10611,.T.);
#11727=FACE_BOUND('',#10612,.T.);
#12667=(
BOUNDED_SURFACE()
B_SPLINE_SURFACE(1,2,((#19849,#19850,#19851,#19852,#19853,#19854,#19855,
#19856,#19857,#19858,#19859,#19860,#19861,#19862,#19863,#19864,#19865,#19866,
#19867,#19868,#19869,#19870,#19871,#19872,#19873,#19874,#19875,#19876,#19877,
#19878,#19879,#19880,#19881,#19882,#19883),(#19884,#19885,#19886,#19887,
#19888,#19889,#19890,#19891,#19892,#19893,#19894,#19895,#19896,#19897,#19898,
#19899,#19900,#19901,#19902,#19903,#19904,#19905,#19906,#19907,#19908,#19909,
#19910,#19911,#19912,#19913,#19914,#19915,#19916,#19917,#19918),(#19919,
#19920,#19921,#19922,#19923,#19924,#19925,#19926,#19927,#19928,#19929,#19930,
#19931,#19932,#19933,#19934,#19935,#19936,#19937,#19938,#19939,#19940,#19941,
#19942,#19943,#19944,#19945,#19946,#19947,#19948,#19949,#19950,#19951,#19952,
#19953)),.RULED_SURF.,.F.,.F.,.F.)
B_SPLINE_SURFACE_WITH_KNOTS((2,1,2),(3,2,2,2,2,2,2,2,2,2,2,2,2,2,2,2,2,
3),(0.,1.,1.08809896316278),(0.,0.05,0.1,0.15,0.2,0.25,0.3,0.35,0.4,0.45,
0.5,0.55,0.6,0.65,0.7,0.75,0.8,0.826757086852854),.UNSPECIFIED.)
GEOMETRIC_REPRESENTATION_ITEM()
RATIONAL_B_SPLINE_SURFACE(((1.,0.951056516295154,1.,0.951056516295154,1.,
0.951056516295154,1.,0.951056516295154,1.,0.951056516295154,1.,0.951056516295154,
1.,0.951056516295154,1.,0.951056516295154,1.,0.951056516295154,1.,0.951056516295154,
1.,0.951056516295154,1.,0.951056516295154,1.,0.951056516295154,1.,0.951056516295154,
1.,0.951056516295154,1.,0.951056516295154,1.,0.973808299112564,0.975649142843891),
(1.,0.951056516295154,1.,0.951056516295154,1.,0.951056516295154,1.,0.951056516295154,
1.,0.951056516295154,1.,0.951056516295154,1.,0.951056516295154,1.,0.951056516295154,
1.,0.951056516295154,1.,0.951056516295154,1.,0.951056516295154,1.,0.951056516295154,
1.,0.951056516295154,1.,0.951056516295154,1.,0.951056516295154,1.,0.951056516295154,
1.,0.973808299112564,0.975649142843891),(1.,0.951056516295154,1.,0.951056516295154,
1.,0.951056516295154,1.,0.951056516295154,1.,0.951056516295154,1.,0.951056516295154,
1.,0.951056516295154,1.,0.951056516295154,1.,0.951056516295154,1.,0.951056516295154,
1.,0.951056516295154,1.,0.951056516295154,1.,0.951056516295154,1.,0.951056516295154,
1.,0.951056516295154,1.,0.951056516295154,1.,0.973808299112564,0.975649142843891)))
REPRESENTATION_ITEM('')
SURFACE()
);
#12756=ADVANCED_FACE('',(#11647,#11648),#1220,.F.);
#12757=ADVANCED_FACE('',(#11649,#11650),#1221,.F.);
#12758=ADVANCED_FACE('',(#11651),#12667,.F.);
#12759=ADVANCED_FACE('',(#11652),#40,.F.);
#12760=ADVANCED_FACE('',(#11653),#1564,.T.);
#12761=ADVANCED_FACE('',(#11654),#1222,.F.);
#12762=ADVANCED_FACE('',(#11655),#1223,.T.);
#12763=ADVANCED_FACE('',(#11656,#11657),#1224,.F.);
#12764=ADVANCED_FACE('',(#11658,#11659),#1225,.F.);
#12765=ADVANCED_FACE('',(#11660,#11661),#1226,.F.);
#12766=ADVANCED_FACE('',(#11662,#11663),#1227,.F.);
#12767=ADVANCED_FACE('',(#11664,#11665),#1228,.F.);
#12768=ADVANCED_FACE('',(#11666,#11667),#1229,.F.);
#12769=ADVANCED_FACE('',(#11668,#11669),#1230,.F.);
#12770=ADVANCED_FACE('',(#11670,#11671),#1231,.F.);
#12771=ADVANCED_FACE('',(#11672,#11673),#1232,.F.);
#12772=ADVANCED_FACE('',(#11674,#11675),#1565,.T.);
#12773=ADVANCED_FACE('',(#11676,#11677),#1566,.T.);
#12774=ADVANCED_FACE('',(#11678,#11679),#1567,.F.);
#12775=ADVANCED_FACE('',(#11680,#11681),#256,.T.);
#12776=ADVANCED_FACE('',(#11682,#11683),#1568,.F.);
#12777=ADVANCED_FACE('',(#11684,#11685),#1569,.F.);
#12778=ADVANCED_FACE('',(#11686,#11687),#21,.F.);
#12779=ADVANCED_FACE('',(#11688,#11689),#1570,.T.);
#12780=ADVANCED_FACE('',(#11690,#11691),#1571,.T.);
#12781=ADVANCED_FACE('',(#11692,#11693),#257,.F.);
#12782=ADVANCED_FACE('',(#11694,#11695),#1572,.T.);
#12783=ADVANCED_FACE('',(#11696,#11697),#1573,.T.);
#12784=ADVANCED_FACE('',(#11698,#11699),#1574,.T.);
#12785=ADVANCED_FACE('',(#11700,#11701),#258,.F.);
#12786=ADVANCED_FACE('',(#11702,#11703),#259,.F.);
#12787=ADVANCED_FACE('',(#11704,#11705),#260,.F.);
#12788=ADVANCED_FACE('',(#11706,#11707),#261,.T.);
#12789=ADVANCED_FACE('',(#11708,#11709),#262,.F.);
#12790=ADVANCED_FACE('',(#11710,#11711),#263,.F.);
#12791=ADVANCED_FACE('',(#11712,#11713),#264,.T.);
#12792=ADVANCED_FACE('',(#11714,#11715),#265,.T.);
#12793=ADVANCED_FACE('',(#11716,#11717),#266,.T.);
#12794=ADVANCED_FACE('',(#11718,#11719),#267,.T.);
#12795=ADVANCED_FACE('',(#11720,#11721),#268,.T.);
#12796=ADVANCED_FACE('',(#11722,#11723),#1575,.T.);
#12797=ADVANCED_FACE('',(#11724,#11725),#269,.F.);
#12798=ADVANCED_FACE('',(#11726,#11727),#270,.F.);
#13503=CLOSED_SHELL('',(#12756,#12757,#12758,#12759,#12760,#12761,#12762,
#12763,#12764,#12765,#12766,#12767,#12768,#12769,#12770,#12771,#12772,#12773,
#12774,#12775,#12776,#12777,#12778,#12779,#12780,#12781,#12782,#12783,#12784,
#12785,#12786,#12787,#12788,#12789,#12790,#12791,#12792,#12793,#12794,#12795,
#12796,#12797,#12798));
#13530=STYLED_ITEM('',(#13557),#13720);
#13557=PRESENTATION_STYLE_ASSIGNMENT((#13584));
#13584=SURFACE_STYLE_USAGE(.BOTH.,#13611);
#13611=SURFACE_SIDE_STYLE('',(#13638));
#13638=SURFACE_STYLE_FILL_AREA(#13665);
#13665=FILL_AREA_STYLE('',(#13692));
#13692=FILL_AREA_STYLE_COLOUR('',#60);
#13720=MANIFOLD_SOLID_BREP('piston',#13503);
#13748=SHAPE_DEFINITION_REPRESENTATION(#45526,#13776);
#13776=SHAPE_REPRESENTATION('piston',(#13802),#45466);
#13802=AXIS2_PLACEMENT_3D('',#19109,#15295,#15296);
#13904=AXIS2_PLACEMENT_3D('',#19839,#15532,#15533);
#13905=AXIS2_PLACEMENT_3D('',#19840,#15534,#15535);
#13906=AXIS2_PLACEMENT_3D('',#19842,#15536,#15537);
#13907=AXIS2_PLACEMENT_3D('',#19844,#15538,#15539);
#13908=AXIS2_PLACEMENT_3D('',#19845,#15540,#15541);
#13909=AXIS2_PLACEMENT_3D('',#19847,#15542,#15543);
#13910=AXIS2_PLACEMENT_3D('',#20003,#15547,#15548);
#13911=AXIS2_PLACEMENT_3D('',#20346,#15551,#15552);
#13912=AXIS2_PLACEMENT_3D('',#20349,#15555,#15556);
#13913=AXIS2_PLACEMENT_3D('',#20352,#15558,#15559);
#13914=AXIS2_PLACEMENT_3D('',#20353,#15560,#15561);
#13915=AXIS2_PLACEMENT_3D('',#20355,#15563,#15564);
#13916=AXIS2_PLACEMENT_3D('',#20356,#15565,#15566);
#13917=AXIS2_PLACEMENT_3D('',#20358,#15567,#15568);
#13918=AXIS2_PLACEMENT_3D('',#20360,#15569,#15570);
#13919=AXIS2_PLACEMENT_3D('',#20361,#15571,#15572);
#13920=AXIS2_PLACEMENT_3D('',#20363,#15573,#15574);
#13921=AXIS2_PLACEMENT_3D('',#20365,#15575,#15576);
#13922=AXIS2_PLACEMENT_3D('',#20366,#15577,#15578);
#13923=AXIS2_PLACEMENT_3D('',#20368,#15579,#15580);
#13924=AXIS2_PLACEMENT_3D('',#20370,#15581,#15582);
#13925=AXIS2_PLACEMENT_3D('',#20371,#15583,#15584);
#13926=AXIS2_PLACEMENT_3D('',#20373,#15585,#15586);
#13927=AXIS2_PLACEMENT_3D('',#20375,#15587,#15588);
#13928=AXIS2_PLACEMENT_3D('',#20376,#15589,#15590);
#13929=AXIS2_PLACEMENT_3D('',#20378,#15591,#15592);
#13930=AXIS2_PLACEMENT_3D('',#20380,#15593,#15594);
#13931=AXIS2_PLACEMENT_3D('',#20381,#15595,#15596);
#13932=AXIS2_PLACEMENT_3D('',#20383,#15597,#15598);
#13933=AXIS2_PLACEMENT_3D('',#20385,#15599,#15600);
#13934=AXIS2_PLACEMENT_3D('',#20386,#15601,#15602);
#13935=AXIS2_PLACEMENT_3D('',#20388,#15603,#15604);
#13936=AXIS2_PLACEMENT_3D('',#20390,#15605,#15606);
#13937=AXIS2_PLACEMENT_3D('',#20391,#15607,#15608);
#13938=AXIS2_PLACEMENT_3D('',#20393,#15609,#15610);
#13939=AXIS2_PLACEMENT_3D('',#20395,#15611,#15612);
#13940=AXIS2_PLACEMENT_3D('',#20396,#15613,#15614);
#13941=AXIS2_PLACEMENT_3D('',#20398,#15615,#15616);
#13942=AXIS2_PLACEMENT_3D('',#20400,#15617,#15618);
#13943=AXIS2_PLACEMENT_3D('',#20401,#15619,#15620);
#13944=AXIS2_PLACEMENT_3D('',#20403,#15621,#15622);
#13945=AXIS2_PLACEMENT_3D('',#20404,#15623,#15624);
#13946=AXIS2_PLACEMENT_3D('',#20405,#15625,#15626);
#13947=AXIS2_PLACEMENT_3D('',#20407,#15627,#15628);
#13948=AXIS2_PLACEMENT_3D('',#20408,#15629,#15630);
#13949=AXIS2_PLACEMENT_3D('',#20410,#15631,#15632);
#13950=AXIS2_PLACEMENT_3D('',#20411,#15633,#15634);
#13951=AXIS2_PLACEMENT_3D('',#20413,#15635,#15636);
#13952=AXIS2_PLACEMENT_3D('',#20414,#15637,#15638);
#13953=AXIS2_PLACEMENT_3D('',#20416,#15639,#15640);
#13954=AXIS2_PLACEMENT_3D('',#20417,#15641,#15642);
#13955=AXIS2_PLACEMENT_3D('',#20419,#15643,#15644);
#13956=AXIS2_PLACEMENT_3D('',#20421,#15645,#15646);
#13957=AXIS2_PLACEMENT_3D('',#20422,#15647,#15648);
#13958=AXIS2_PLACEMENT_3D('',#20423,#15649,#15650);
#13959=AXIS2_PLACEMENT_3D('',#20424,#15651,#15652);
#13960=AXIS2_PLACEMENT_3D('',#20426,#15653,#15654);
#13961=AXIS2_PLACEMENT_3D('',#20428,#15655,#15656);
#13962=AXIS2_PLACEMENT_3D('',#20429,#15657,#15658);
#13963=AXIS2_PLACEMENT_3D('',#20430,#15659,#15660);
#13964=AXIS2_PLACEMENT_3D('',#20432,#15661,#15662);
#13965=AXIS2_PLACEMENT_3D('',#20433,#15663,#15664);
#13966=AXIS2_PLACEMENT_3D('',#20435,#15665,#15666);
#13967=AXIS2_PLACEMENT_3D('',#20437,#15667,#15668);
#13968=AXIS2_PLACEMENT_3D('',#20438,#15669,#15670);
#13969=AXIS2_PLACEMENT_3D('',#20440,#15671,#15672);
#13970=AXIS2_PLACEMENT_3D('',#20441,#15673,#15674);
#13971=AXIS2_PLACEMENT_3D('',#20442,#15675,#15676);
#13972=AXIS2_PLACEMENT_3D('',#20443,#15677,#15678);
#13973=AXIS2_PLACEMENT_3D('',#20444,#15679,#15680);
#13974=AXIS2_PLACEMENT_3D('',#20445,#15681,#15682);
#13975=AXIS2_PLACEMENT_3D('',#20446,#15683,#15684);
#13976=AXIS2_PLACEMENT_3D('',#20447,#15685,#15686);
#13977=AXIS2_PLACEMENT_3D('',#20448,#15687,#15688);
#13978=AXIS2_PLACEMENT_3D('',#20449,#15689,#15690);
#13979=AXIS2_PLACEMENT_3D('',#20450,#15691,#15692);
#13980=AXIS2_PLACEMENT_3D('',#20451,#15693,#15694);
#13981=AXIS2_PLACEMENT_3D('',#20452,#15695,#15696);
#13982=AXIS2_PLACEMENT_3D('',#20454,#15697,#15698);
#13983=AXIS2_PLACEMENT_3D('',#20456,#15699,#15700);
#13984=AXIS2_PLACEMENT_3D('',#20457,#15701,#15702);
#15295=DIRECTION('',(0.,0.,1.));
#15296=DIRECTION('',(1.,0.,0.));
#15532=DIRECTION('',(0.,0.,1.));
#15533=DIRECTION('',(1.,0.,0.));
#15534=DIRECTION('',(4.16495833440966E-16,0.,1.));
#15535=DIRECTION('',(1.,0.,0.));
#15536=DIRECTION('',(4.16495833440966E-16,0.,1.));
#15537=DIRECTION('',(1.,0.,0.));
#15538=DIRECTION('',(0.,0.,-1.));
#15539=DIRECTION('',(-1.,0.,0.));
#15540=DIRECTION('',(-4.16495833440966E-16,0.,-1.));
#15541=DIRECTION('',(-1.,0.,0.));
#15542=DIRECTION('',(-4.16495833440966E-16,0.,-1.));
#15543=DIRECTION('',(-1.,0.,0.));
#15544=DIRECTION('',(0.86602540378444,0.,-0.5));
#15545=DIRECTION('',(0.493314209934358,-0.711787250712482,0.500000000000007));
#15546=DIRECTION('',(-0.493314209934064,0.711787250712696,-0.499999999999992));
#15547=DIRECTION('',(0.0139418328291082,0.0429085493761317,-0.998981722399265));
#15548=DIRECTION('',(0.999902807845662,-0.000610909849002805,0.0139284475630859));
#15549=DIRECTION('',(-0.86602540378444,0.,-0.5));
#15550=DIRECTION('',(-0.493317861910604,0.711784820259979,0.4999998567674));
#15551=DIRECTION('',(1.5963568800503E-17,-8.85021464712618E-18,-1.));
#15552=DIRECTION('',(-1.,0.,-1.5963568800503E-17));
#15553=DIRECTION('',(0.,0.,-1.));
#15554=DIRECTION('',(4.89971376945695E-6,3.39581651649945E-6,0.999999999982231));
#15555=DIRECTION('',(0.821901121609115,0.569630183801455,0.));
#15556=DIRECTION('',(-0.569630183801455,0.821901121609115,0.));
#15557=DIRECTION('',(0.,0.,-1.));
#15558=DIRECTION('',(0.821901121609115,0.569630183801455,0.));
#15559=DIRECTION('',(-0.569630183801455,0.821901121609115,0.));
#15560=DIRECTION('',(0.,-1.,0.));
#15561=DIRECTION('',(0.,0.,-1.));
#15562=DIRECTION('',(0.,0.,1.));
#15563=DIRECTION('',(0.,0.,-1.));
#15564=DIRECTION('',(-1.,0.,0.));
#15565=DIRECTION('',(-1.22464679914735E-16,0.,-1.));
#15566=DIRECTION('',(-1.,0.,2.06514699521048E-16));
#15567=DIRECTION('',(1.22464679914735E-16,0.,1.));
#15568=DIRECTION('',(-1.,0.,1.80700362080917E-16));
#15569=DIRECTION('',(0.,0.,1.));
#15570=DIRECTION('',(1.,0.,0.));
#15571=DIRECTION('',(1.22464679914735E-16,0.,1.));
#15572=DIRECTION('',(1.,0.,-2.06514699521048E-16));
#15573=DIRECTION('',(-1.22464679914735E-16,0.,-1.));
#15574=DIRECTION('',(1.,0.,-1.80700362080917E-16));
#15575=DIRECTION('',(0.,0.,-1.));
#15576=DIRECTION('',(-1.,0.,0.));
#15577=DIRECTION('',(-1.22464679914735E-16,0.,-1.));
#15578=DIRECTION('',(-1.,0.,0.));
#15579=DIRECTION('',(-1.22464679914735E-16,0.,-1.));
#15580=DIRECTION('',(-1.,0.,0.));
#15581=DIRECTION('',(0.,0.,1.));
#15582=DIRECTION('',(1.,0.,0.));
#15583=DIRECTION('',(1.22464679914735E-16,0.,1.));
#15584=DIRECTION('',(1.,0.,0.));
#15585=DIRECTION('',(-1.22464679914735E-16,0.,-1.));
#15586=DIRECTION('',(1.,0.,0.));
#15587=DIRECTION('',(0.,0.,-1.));
#15588=DIRECTION('',(-1.,0.,0.));
#15589=DIRECTION('',(-1.22464679914735E-16,0.,-1.));
#15590=DIRECTION('',(-1.,0.,0.));
#15591=DIRECTION('',(1.22464679914735E-16,0.,1.));
#15592=DIRECTION('',(-1.,0.,0.));
#15593=DIRECTION('',(0.,0.,-1.));
#15594=DIRECTION('',(-1.,0.,0.));
#15595=DIRECTION('',(-1.22464679914735E-16,0.,-1.));
#15596=DIRECTION('',(-1.,0.,0.));
#15597=DIRECTION('',(-1.22464679914735E-16,0.,-1.));
#15598=DIRECTION('',(-1.,0.,0.));
#15599=DIRECTION('',(0.,0.,1.));
#15600=DIRECTION('',(1.,0.,0.));
#15601=DIRECTION('',(1.22464679914735E-16,0.,1.));
#15602=DIRECTION('',(1.,0.,0.));
#15603=DIRECTION('',(-1.22464679914735E-16,0.,-1.));
#15604=DIRECTION('',(1.,0.,0.));
#15605=DIRECTION('',(0.,0.,1.));
#15606=DIRECTION('',(1.,0.,0.));
#15607=DIRECTION('',(-1.22464679914735E-16,0.,-1.));
#15608=DIRECTION('',(-1.,0.,0.));
#15609=DIRECTION('',(-1.22464679914735E-16,0.,-1.));
#15610=DIRECTION('',(-1.,0.,0.));
#15611=DIRECTION('',(0.,0.,1.));
#15612=DIRECTION('',(1.,0.,0.));
#15613=DIRECTION('',(-1.22464679914735E-16,0.,-1.));
#15614=DIRECTION('',(-1.,0.,1.20466908053945E-16));
#15615=DIRECTION('',(1.22464679914735E-16,0.,1.));
#15616=DIRECTION('',(1.,0.,-1.21972744404619E-16));
#15617=DIRECTION('',(0.,0.,-1.));
#15618=DIRECTION('',(-1.,0.,0.));
#15619=DIRECTION('',(1.22464679914735E-16,0.,1.));
#15620=DIRECTION('',(-1.,0.,0.));
#15621=DIRECTION('',(0.,0.,-1.));
#15622=DIRECTION('',(-1.,0.,0.));
#15623=DIRECTION('',(1.22464679914735E-16,0.,1.));
#15624=DIRECTION('',(1.,0.,0.));
#15625=DIRECTION('',(-1.22464679914735E-16,0.,-1.));
#15626=DIRECTION('',(-1.,0.,0.));
#15627=DIRECTION('',(0.,0.,-1.));
#15628=DIRECTION('',(-1.,0.,0.));
#15629=DIRECTION('',(-1.22464679914735E-16,0.,-1.));
#15630=DIRECTION('',(1.,0.,-1.22876246215024E-16));
#15631=DIRECTION('',(0.,0.,-1.));
#15632=DIRECTION('',(-1.,0.,0.));
#15633=DIRECTION('',(-1.22464679914735E-16,0.,-1.));
#15634=DIRECTION('',(-1.,0.,0.));
#15635=DIRECTION('',(0.,0.,-1.));
#15636=DIRECTION('',(-1.,0.,0.));
#15637=DIRECTION('',(1.22464679914735E-16,0.,1.));
#15638=DIRECTION('',(1.,0.,0.));
#15639=DIRECTION('',(0.,0.,-1.));
#15640=DIRECTION('',(-1.,0.,0.));
#15641=DIRECTION('',(-1.22464679914735E-16,0.,-1.));
#15642=DIRECTION('',(1.,0.,0.));
#15643=DIRECTION('',(-1.22464679914735E-16,0.,-1.));
#15644=DIRECTION('',(-1.,0.,0.));
#15645=DIRECTION('',(0.,0.,1.));
#15646=DIRECTION('',(1.,0.,0.));
#15647=DIRECTION('',(0.,0.,-1.));
#15648=DIRECTION('',(-1.,0.,0.));
#15649=DIRECTION('',(0.,0.,-1.));
#15650=DIRECTION('',(-1.,0.,0.));
#15651=DIRECTION('',(-1.22464679914735E-16,0.,-1.));
#15652=DIRECTION('',(-1.,0.,0.));
#15653=DIRECTION('',(-1.22464679914735E-16,0.,-1.));
#15654=DIRECTION('',(1.,0.,0.));
#15655=DIRECTION('',(0.,0.,-1.));
#15656=DIRECTION('',(-1.,0.,0.));
#15657=DIRECTION('',(0.,0.,-1.));
#15658=DIRECTION('',(-1.,0.,0.));
#15659=DIRECTION('',(1.22464679914735E-16,0.,1.));
#15660=DIRECTION('',(1.,0.,-1.75224593533011E-16));
#15661=DIRECTION('',(0.,0.,-1.));
#15662=DIRECTION('',(-1.,0.,0.));
#15663=DIRECTION('',(1.22464679914735E-16,0.,1.));
#15664=DIRECTION('',(-1.,0.,2.0900282843094E-16));
#15665=DIRECTION('',(-1.22464679914735E-16,0.,-1.));
#15666=DIRECTION('',(1.,0.,-2.0900282843094E-16));
#15667=DIRECTION('',(0.,0.,-1.));
#15668=DIRECTION('',(-1.,0.,0.));
#15669=DIRECTION('',(-1.22464679914735E-16,0.,-1.));
#15670=DIRECTION('',(-1.,0.,1.75224593533011E-16));
#15671=DIRECTION('',(0.,0.,1.));
#15672=DIRECTION('',(1.,0.,0.));
#15673=DIRECTION('',(0.,0.,-1.));
#15674=DIRECTION('',(-1.,0.,0.));
#15675=DIRECTION('',(0.,0.,1.));
#15676=DIRECTION('',(1.,0.,0.));
#15677=DIRECTION('',(0.,0.,1.));
#15678=DIRECTION('',(1.,0.,0.));
#15679=DIRECTION('',(0.,0.,1.));
#15680=DIRECTION('',(1.,0.,0.));
#15681=DIRECTION('',(0.,0.,-1.));
#15682=DIRECTION('',(-1.,0.,0.));
#15683=DIRECTION('',(0.,0.,1.));
#15684=DIRECTION('',(1.,0.,0.));
#15685=DIRECTION('',(0.,0.,-1.));
#15686=DIRECTION('',(-1.,0.,0.));
#15687=DIRECTION('',(0.,0.,-1.));
#15688=DIRECTION('',(-1.,0.,0.));
#15689=DIRECTION('',(0.,0.,1.));
#15690=DIRECTION('',(1.,0.,0.));
#15691=DIRECTION('',(0.,0.,1.));
#15692=DIRECTION('',(1.,0.,0.));
#15693=DIRECTION('',(0.,0.,1.));
#15694=DIRECTION('',(1.,0.,0.));
#15695=DIRECTION('',(-4.16495833440966E-16,0.,-1.));
#15696=DIRECTION('',(1.,0.,0.));
#15697=DIRECTION('',(4.16495833440966E-16,0.,1.));
#15698=DIRECTION('',(-1.,0.,0.));
#15699=DIRECTION('',(0.,0.,-1.));
#15700=DIRECTION('',(-1.,0.,0.));
#15701=DIRECTION('',(0.,0.,1.));
#15702=DIRECTION('',(1.,0.,0.));
#19109=CARTESIAN_POINT('',(0.,0.,0.));
#19839=CARTESIAN_POINT('',(0.00604745574900122,0.,0.06762567913));
#19840=CARTESIAN_POINT('',(8.28175714867204E-18,0.,0.06762567913));
#19841=CARTESIAN_POINT('',(0.00450000000000001,0.,0.06762567913));
#19842=CARTESIAN_POINT('',(6.5911382126792E-18,0.,0.06762567913));
#19843=CARTESIAN_POINT('',(0.00380000000000001,0.,0.06762567913));
#19844=CARTESIAN_POINT('',(0.00604745574900122,0.,0.06622567913));
#19845=CARTESIAN_POINT('',(8.11030659679141E-18,0.,0.06622567913));
#19846=CARTESIAN_POINT('',(-0.00449999999999999,0.,0.06622567913));
#19847=CARTESIAN_POINT('',(6.00804404586185E-18,0.,0.06622567913));
#19848=CARTESIAN_POINT('',(-0.00379999999999999,0.,0.06622567913));
#19849=CARTESIAN_POINT('',(-0.00748201094464286,0.,0.0501919291324776));
#19850=CARTESIAN_POINT('',(-0.00748201094464285,0.00243105272334464,0.0501012148467632));
#19851=CARTESIAN_POINT('',(-0.00605307400631542,0.00439781569075195,0.050010500561049));
#19852=CARTESIAN_POINT('',(-0.00462413706798799,0.00636457865815926,0.0499197862753347));
#19853=CARTESIAN_POINT('',(-0.00231206853399399,0.00711581526389425,0.0498290719896204));
#19854=CARTESIAN_POINT('',(5.60947406115009E-18,0.00786705186962924,0.0497383577039061));
#19855=CARTESIAN_POINT('',(0.00231206853399401,0.00711581526389425,0.0496476434181919));
#19856=CARTESIAN_POINT('',(0.004624137067988,0.00636457865815926,0.0495569291324775));
#19857=CARTESIAN_POINT('',(0.00605307400631544,0.00439781569075195,0.0494662148467633));
#19858=CARTESIAN_POINT('',(0.00748201094464287,0.00243105272334464,0.049375500561049));
#19859=CARTESIAN_POINT('',(0.00748201094464287,9.16282075454235E-19,0.0492847862753347));
#19860=CARTESIAN_POINT('',(0.00748201094464287,-0.00243105272334463,0.0491940719896204));
#19861=CARTESIAN_POINT('',(0.00605307400631544,-0.00439781569075195,0.0491033577039062));
#19862=CARTESIAN_POINT('',(0.004624137067988,-0.00636457865815926,0.0490126434181918));
#19863=CARTESIAN_POINT('',(0.00231206853399401,-0.00711581526389425,0.0489219291324776));
#19864=CARTESIAN_POINT('',(7.42525307968667E-18,-0.00786705186962924,0.0488312148467633));
#19865=CARTESIAN_POINT('',(-0.00231206853399399,-0.00711581526389425,0.048740500561049));
#19866=CARTESIAN_POINT('',(-0.00462413706798798,-0.00636457865815926,0.0486497862753347));
#19867=CARTESIAN_POINT('',(-0.00605307400631542,-0.00439781569075195,0.0485590719896204));
#19868=CARTESIAN_POINT('',(-0.00748201094464285,-0.00243105272334464,0.0484683577039061));
#19869=CARTESIAN_POINT('',(-0.00748201094464286,0.,0.0483776434181919));
#19870=CARTESIAN_POINT('',(-0.00748201094464285,0.00243105272334464,0.0482869291324776));
#19871=CARTESIAN_POINT('',(-0.00605307400631542,0.00439781569075195,0.0481962148467633));
#19872=CARTESIAN_POINT('',(-0.00462413706798799,0.00636457865815926,0.048105500561049));
#19873=CARTESIAN_POINT('',(-0.00231206853399399,0.00711581526389425,0.0480147862753347));
#19874=CARTESIAN_POINT('',(5.38728814187621E-18,0.00786705186962924,0.0479240719896205));
#19875=CARTESIAN_POINT('',(0.00231206853399401,0.00711581526389425,0.0478333577039062));
#19876=CARTESIAN_POINT('',(0.004624137067988,0.00636457865815926,0.0477426434181919));
#19877=CARTESIAN_POINT('',(0.00605307400631544,0.00439781569075195,0.0476519291324776));
#19878=CARTESIAN_POINT('',(0.00748201094464287,0.00243105272334464,0.0475612148467632));
#19879=CARTESIAN_POINT('',(0.00748201094464287,9.16282075454235E-19,0.047470500561049));
#19880=CARTESIAN_POINT('',(0.00748201094464287,-0.00243105272334463,0.0473797862753347));
#19881=CARTESIAN_POINT('',(0.00605307400631544,-0.00439781569075195,0.0472890719896204));
#19882=CARTESIAN_POINT('',(0.00530625606780677,-0.00542572239919884,0.0472416611809043));
#19883=CARTESIAN_POINT('',(0.00426197926959799,-0.00614947318729602,0.0471918228596965));
#19884=CARTESIAN_POINT('',(-0.0065,0.,0.0496249648492409));
#19885=CARTESIAN_POINT('',(-0.0065,0.00211197802551389,0.0495342505635266));
#19886=CARTESIAN_POINT('',(-0.00525861046343716,0.00382060413990108,0.0494435362778123));
#19887=CARTESIAN_POINT('',(-0.00401722092687431,0.00552923025428826,0.049352821992098));
#19888=CARTESIAN_POINT('',(-0.00200861046343716,0.0061818673559185,0.0492621077063837));
#19889=CARTESIAN_POINT('',(5.60326625583903E-18,0.00683450445754873,0.0491713934206694));
#19890=CARTESIAN_POINT('',(0.00200861046343717,0.0061818673559185,0.0490806791349552));
#19891=CARTESIAN_POINT('',(0.00401722092687432,0.00552923025428826,0.0489899648492409));
#19892=CARTESIAN_POINT('',(0.00525861046343717,0.00382060413990108,0.0488992505635266));
#19893=CARTESIAN_POINT('',(0.00650000000000001,0.00211197802551389,0.0488085362778123));
#19894=CARTESIAN_POINT('',(0.0065,7.9602041944578E-19,0.048717821992098));
#19895=CARTESIAN_POINT('',(0.00650000000000001,-0.00211197802551389,0.0486271077063837));
#19896=CARTESIAN_POINT('',(0.00525861046343717,-0.00382060413990108,0.0485363934206694));
#19897=CARTESIAN_POINT('',(0.00401722092687432,-0.00552923025428826,0.0484456791349552));
#19898=CARTESIAN_POINT('',(0.00200861046343717,-0.0061818673559185,0.0483549648492409));
#19899=CARTESIAN_POINT('',(7.16614409774116E-18,-0.00683450445754873,0.0482642505635266));
#19900=CARTESIAN_POINT('',(-0.00200861046343716,-0.0061818673559185,0.0481735362778123));
#19901=CARTESIAN_POINT('',(-0.00401722092687431,-0.00552923025428826,0.048082821992098));
#19902=CARTESIAN_POINT('',(-0.00525861046343716,-0.00382060413990108,0.0479921077063837));
#19903=CARTESIAN_POINT('',(-0.0065,-0.00211197802551389,0.0479013934206695));
#19904=CARTESIAN_POINT('',(-0.0065,0.,0.0478106791349552));
#19905=CARTESIAN_POINT('',(-0.0065,0.00211197802551389,0.0477199648492408));
#19906=CARTESIAN_POINT('',(-0.00525861046343716,0.00382060413990108,0.0476292505635266));
#19907=CARTESIAN_POINT('',(-0.00401722092687431,0.00552923025428826,0.0475385362778122));
#19908=CARTESIAN_POINT('',(-0.00200861046343716,0.0061818673559185,0.047447821992098));
#19909=CARTESIAN_POINT('',(5.38108033656515E-18,0.00683450445754873,0.0473571077063837));
#19910=CARTESIAN_POINT('',(0.00200861046343717,0.0061818673559185,0.0472663934206695));
#19911=CARTESIAN_POINT('',(0.00401722092687432,0.00552923025428826,0.0471756791349551));
#19912=CARTESIAN_POINT('',(0.00525861046343717,0.00382060413990108,0.0470849648492409));
#19913=CARTESIAN_POINT('',(0.00650000000000001,0.00211197802551389,0.0469942505635266));
#19914=CARTESIAN_POINT('',(0.0065,7.9602041944578E-19,0.0469035362778123));
#19915=CARTESIAN_POINT('',(0.00650000000000001,-0.00211197802551389,0.046812821992098));
#19916=CARTESIAN_POINT('',(0.00525861046343717,-0.00382060413990108,0.0467221077063837));
#19917=CARTESIAN_POINT('',(0.00460981208072669,-0.00471359850389472,0.0466746968976677));
#19918=CARTESIAN_POINT('',(0.00370259619470649,-0.00534235729046131,0.0466248585764598));
#19919=CARTESIAN_POINT('',(-0.00641348585396246,0.,0.0495750158837374));
#19920=CARTESIAN_POINT('',(-0.00641348585396245,0.00208386787546353,0.0494843015980231));
#19921=CARTESIAN_POINT('',(-0.00518861904903895,0.00376975240074554,0.0493935873123088));
#19922=CARTESIAN_POINT('',(-0.00396375224411544,0.00545563692602755,0.0493028730265945));
#19923=CARTESIAN_POINT('',(-0.00198187612205772,0.00609958751357779,0.0492121587408802));
#19924=CARTESIAN_POINT('',(5.6027193546276E-18,0.00674353810112803,0.0491214444551659));
#19925=CARTESIAN_POINT('',(0.00198187612205773,0.00609958751357779,0.0490307301694517));
#19926=CARTESIAN_POINT('',(0.00396375224411545,0.00545563692602755,0.0489400158837374));
#19927=CARTESIAN_POINT('',(0.00518861904903896,0.00376975240074554,0.0488493015980231));
#19928=CARTESIAN_POINT('',(0.00641348585396247,0.00208386787546353,0.0487585873123088));
#19929=CARTESIAN_POINT('',(0.00641348585396247,7.85425492243196E-19,0.0486678730265945));
#19930=CARTESIAN_POINT('',(0.00641348585396247,-0.00208386787546353,0.0485771587408802));
#19931=CARTESIAN_POINT('',(0.00518861904903896,-0.00376975240074554,0.048486444455166));
#19932=CARTESIAN_POINT('',(0.00396375224411545,-0.00545563692602755,0.0483957301694517));
#19933=CARTESIAN_POINT('',(0.00198187612205773,-0.00609958751357779,0.0483050158837374));
#19934=CARTESIAN_POINT('',(7.1433168650856E-18,-0.00674353810112803,0.0482143015980231));
#19935=CARTESIAN_POINT('',(-0.00198187612205772,-0.00609958751357779,0.0481235873123088));
#19936=CARTESIAN_POINT('',(-0.00396375224411544,-0.00545563692602755,0.0480328730265945));
#19937=CARTESIAN_POINT('',(-0.00518861904903895,-0.00376975240074554,0.0479421587408802));
#19938=CARTESIAN_POINT('',(-0.00641348585396245,-0.00208386787546353,0.047851444455166));
#19939=CARTESIAN_POINT('',(-0.00641348585396246,0.,0.0477607301694517));
#19940=CARTESIAN_POINT('',(-0.00641348585396245,0.00208386787546353,0.0476700158837374));
#19941=CARTESIAN_POINT('',(-0.00518861904903895,0.00376975240074554,0.0475793015980231));
#19942=CARTESIAN_POINT('',(-0.00396375224411544,0.00545563692602755,0.0474885873123088));
#19943=CARTESIAN_POINT('',(-0.00198187612205772,0.00609958751357779,0.0473978730265945));
#19944=CARTESIAN_POINT('',(5.38053343535374E-18,0.00674353810112803,0.0473071587408802));
#19945=CARTESIAN_POINT('',(0.00198187612205773,0.00609958751357779,0.047216444455166));
#19946=CARTESIAN_POINT('',(0.00396375224411545,0.00545563692602755,0.0471257301694517));
#19947=CARTESIAN_POINT('',(0.00518861904903896,0.00376975240074554,0.0470350158837374));
#19948=CARTESIAN_POINT('',(0.00641348585396247,0.00208386787546353,0.0469443015980231));
#19949=CARTESIAN_POINT('',(0.00641348585396247,7.85425492243196E-19,0.0468535873123088));
#19950=CARTESIAN_POINT('',(0.00641348585396247,-0.00208386787546353,0.0467628730265945));
#19951=CARTESIAN_POINT('',(0.00518861904903896,-0.00376975240074554,0.0466721587408802));
#19952=CARTESIAN_POINT('',(0.00454845608756398,-0.00465086112707498,0.0466247479321641));
#19953=CARTESIAN_POINT('',(0.00365331512579774,-0.00527125121679797,0.0465749096109563));
#19954=CARTESIAN_POINT('',(-0.00699100547232143,0.,0.0499084469908592));
#19955=CARTESIAN_POINT('',(-0.00748201094464286,0.,0.0501919291324776));
#19956=CARTESIAN_POINT('',(-0.0065,0.,0.0496249648492409));
#19957=CARTESIAN_POINT('',(-0.00748201094464286,0.,0.0501919291324776));
#19958=CARTESIAN_POINT('',(-0.00748201094464285,0.00243105272334464,0.0501012148467632));
#19959=CARTESIAN_POINT('',(-0.00605307400631542,0.00439781569075195,0.050010500561049));
#19960=CARTESIAN_POINT('',(-0.00462413706798799,0.00636457865815926,0.0499197862753347));
#19961=CARTESIAN_POINT('',(-0.00231206853399399,0.00711581526389425,0.0498290719896204));
#19962=CARTESIAN_POINT('',(5.60947406115009E-18,0.00786705186962924,0.0497383577039061));
#19963=CARTESIAN_POINT('',(0.00231206853399401,0.00711581526389425,0.0496476434181919));
#19964=CARTESIAN_POINT('',(0.004624137067988,0.00636457865815926,0.0495569291324775));
#19965=CARTESIAN_POINT('',(0.00605307400631544,0.00439781569075195,0.0494662148467633));
#19966=CARTESIAN_POINT('',(0.00748201094464287,0.00243105272334464,0.049375500561049));
#19967=CARTESIAN_POINT('',(0.00748201094464287,9.16282075454235E-19,0.0492847862753347));
#19968=CARTESIAN_POINT('',(0.00748201094464287,-0.00243105272334463,0.0491940719896204));
#19969=CARTESIAN_POINT('',(0.00605307400631544,-0.00439781569075195,0.0491033577039062));
#19970=CARTESIAN_POINT('',(0.004624137067988,-0.00636457865815926,0.0490126434181918));
#19971=CARTESIAN_POINT('',(0.00231206853399401,-0.00711581526389425,0.0489219291324776));
#19972=CARTESIAN_POINT('',(7.42525307968667E-18,-0.00786705186962924,0.0488312148467633));
#19973=CARTESIAN_POINT('',(-0.00231206853399399,-0.00711581526389425,0.048740500561049));
#19974=CARTESIAN_POINT('',(-0.00462413706798798,-0.00636457865815926,0.0486497862753347));
#19975=CARTESIAN_POINT('',(-0.00605307400631542,-0.00439781569075195,0.0485590719896204));
#19976=CARTESIAN_POINT('',(-0.00748201094464285,-0.00243105272334464,0.0484683577039061));
#19977=CARTESIAN_POINT('',(-0.00748201094464286,0.,0.0483776434181919));
#19978=CARTESIAN_POINT('',(-0.00748201094464285,0.00243105272334464,0.0482869291324776));
#19979=CARTESIAN_POINT('',(-0.00605307400631542,0.00439781569075195,0.0481962148467633));
#19980=CARTESIAN_POINT('',(-0.00462413706798799,0.00636457865815926,0.048105500561049));
#19981=CARTESIAN_POINT('',(-0.00231206853399399,0.00711581526389425,0.0480147862753347));
#19982=CARTESIAN_POINT('',(5.38728814187621E-18,0.00786705186962924,0.0479240719896205));
#19983=CARTESIAN_POINT('',(0.00231206853399401,0.00711581526389425,0.0478333577039062));
#19984=CARTESIAN_POINT('',(0.004624137067988,0.00636457865815926,0.0477426434181919));
#19985=CARTESIAN_POINT('',(0.00605307400631544,0.00439781569075195,0.0476519291324776));
#19986=CARTESIAN_POINT('',(0.00748201094464287,0.00243105272334464,0.0475612148467632));
#19987=CARTESIAN_POINT('',(0.00748201094464287,9.16282075454235E-19,0.047470500561049));
#19988=CARTESIAN_POINT('',(0.00748201094464287,-0.00243105272334463,0.0473797862753347));
#19989=CARTESIAN_POINT('',(0.00605307400631544,-0.00439781569075195,0.0472890719896204));
#19990=CARTESIAN_POINT('',(0.00530625606780689,-0.00542572239919866,0.0472416611809044));
#19991=CARTESIAN_POINT('',(0.00426197926959833,-0.00614947318729578,0.0471918228596965));
#19992=CARTESIAN_POINT('',(0.00426197926959833,-0.00614947318729578,0.0471918228596965));
#19993=CARTESIAN_POINT('',(0.00398228773215241,-0.00574591523887855,0.0469083407180782));
#19994=CARTESIAN_POINT('',(0.00370259619470649,-0.00534235729046131,0.0466248585764598));
#19995=CARTESIAN_POINT('',(0.00367795566025212,-0.00530680425362964,0.046599884093708));
#19996=CARTESIAN_POINT('',(0.00365331512579812,-0.00527125121679776,0.0465749096109563));
#19997=CARTESIAN_POINT('',(0.00365331512579852,-0.00527125121679756,0.0465749096109564));
#19998=CARTESIAN_POINT('',(0.00418300421785061,-0.00498093574494503,0.046638839317779));
#19999=CARTESIAN_POINT('',(0.00509595215042321,-0.00414814728430873,0.0466991834499751));
#20000=CARTESIAN_POINT('',(0.00573004291196533,-0.00312785079813037,0.0467584423785249));
#20001=CARTESIAN_POINT('',(0.00596966594774492,-0.00257159259454815,0.04678567913));
#20002=CARTESIAN_POINT('',(0.00596966594774489,-0.00257159259454823,0.04678567913));
#20003=CARTESIAN_POINT('',(-1.22293354860711E-5,3.97877174541167E-6,0.0468128222162991));
#20004=CARTESIAN_POINT('',(0.0065,7.9602041944578E-19,0.0469035362778123));
#20005=CARTESIAN_POINT('',(-0.0065,0.,0.0478106791349552));
#20006=CARTESIAN_POINT('',(-0.00650000000000001,0.00211197802551388,0.0477199648492409));
#20007=CARTESIAN_POINT('',(-0.00525861046343716,0.00382060413990108,0.0476292505635266));
#20008=CARTESIAN_POINT('',(-0.00401722092687431,0.00552923025428826,0.0475385362778122));
#20009=CARTESIAN_POINT('',(-0.00200861046343716,0.0061818673559185,0.047447821992098));
#20010=CARTESIAN_POINT('',(5.38108033656515E-18,0.00683450445754873,0.0473571077063837));
#20011=CARTESIAN_POINT('',(0.00200861046343717,0.0061818673559185,0.0472663934206695));
#20012=CARTESIAN_POINT('',(0.00401722092687432,0.00552923025428826,0.0471756791349551));
#20013=CARTESIAN_POINT('',(0.00525861046343717,0.00382060413990108,0.0470849648492409));
#20014=CARTESIAN_POINT('',(0.00649999999999998,0.00211197802551393,0.0469942505635266));
#20015=CARTESIAN_POINT('',(0.0065,7.96020419445779E-19,0.0469035362778123));
#20016=CARTESIAN_POINT('',(-0.0065,0.,0.0478106791349552));
#20017=CARTESIAN_POINT('',(0.0065,7.96020419445781E-19,0.0487178219920981));
#20018=CARTESIAN_POINT('',(0.00650000000000003,-0.00211197802551387,0.0486271077063837));
#20019=CARTESIAN_POINT('',(0.00525861046343717,-0.00382060413990108,0.0485363934206694));
#20020=CARTESIAN_POINT('',(0.00401722092687432,-0.00552923025428826,0.0484456791349552));
#20021=CARTESIAN_POINT('',(0.00200861046343717,-0.0061818673559185,0.0483549648492409));
#20022=CARTESIAN_POINT('',(7.16614409774116E-18,-0.00683450445754873,0.0482642505635266));
#20023=CARTESIAN_POINT('',(-0.00200861046343716,-0.0061818673559185,0.0481735362778123));
#20024=CARTESIAN_POINT('',(-0.00401722092687431,-0.00552923025428826,0.048082821992098));
#20025=CARTESIAN_POINT('',(-0.00525861046343716,-0.00382060413990108,0.0479921077063837));
#20026=CARTESIAN_POINT('',(-0.00649999999999999,-0.00211197802551391,0.0479013934206695));
#20027=CARTESIAN_POINT('',(-0.0065,0.,0.0478106791349552));
#20028=CARTESIAN_POINT('',(0.0065,7.9602041944578E-19,0.048717821992098));
#20029=CARTESIAN_POINT('',(-0.0065,0.,0.0496249648492409));
#20030=CARTESIAN_POINT('',(-0.0065,0.00211197802551389,0.0495342505635266));
#20031=CARTESIAN_POINT('',(-0.00525861046343716,0.00382060413990108,0.0494435362778123));
#20032=CARTESIAN_POINT('',(-0.00401722092687431,0.00552923025428826,0.049352821992098));
#20033=CARTESIAN_POINT('',(-0.00200861046343716,0.0061818673559185,0.0492621077063837));
#20034=CARTESIAN_POINT('',(5.60326625583903E-18,0.00683450445754873,0.0491713934206694));
#20035=CARTESIAN_POINT('',(0.00200861046343717,0.0061818673559185,0.0490806791349552));
#20036=CARTESIAN_POINT('',(0.00401722092687432,0.00552923025428826,0.0489899648492409));
#20037=CARTESIAN_POINT('',(0.00525861046343717,0.00382060413990108,0.0488992505635266));
#20038=CARTESIAN_POINT('',(0.0065,0.00211197802551392,0.0488085362778123));
#20039=CARTESIAN_POINT('',(0.0065,7.9602041944578E-19,0.048717821992098));
#20040=CARTESIAN_POINT('',(-0.0065,0.,0.05098567913));
#20041=CARTESIAN_POINT('',(-0.0065,0.00139216394854201,0.0509258825049104));
#20042=CARTESIAN_POINT('',(-0.00601209861219997,0.00283854168444359,0.0508578508580355));
#20043=CARTESIAN_POINT('',(-0.00473881207941318,0.00450353441535566,0.0507671294297172));
#20044=CARTESIAN_POINT('',(-0.00421228132056244,0.00500154670113435,0.0507346711453865));
#20045=CARTESIAN_POINT('',(-0.0030273902334642,0.00579600653049259,0.0506702885995784));
#20046=CARTESIAN_POINT('',(-0.00237885749509726,0.00608954574355769,0.0506395433453287));
#20047=CARTESIAN_POINT('',(-0.00102560939713424,0.00645675272171483,0.050578426998065));
#20048=CARTESIAN_POINT('',(-0.00030367301496546,0.0065319158651834,0.0505458223968087));
#20049=CARTESIAN_POINT('',(0.00111920072308763,0.00644247870864103,0.0504815615671662));
#20050=CARTESIAN_POINT('',(0.00180859004388786,0.00628280413851949,0.0504513811063915));
#20051=CARTESIAN_POINT('',(0.00311059239441925,0.00575055134275219,0.0503896801606666));
#20052=CARTESIAN_POINT('',(0.00373007126500205,0.00537063786359636,0.0503569608419805));
#20053=CARTESIAN_POINT('',(0.0048044795422359,0.00443555622578788,0.0502928821077617));
#20054=CARTESIAN_POINT('',(0.00525317896866053,0.00389249931724978,0.0502631287087374));
#20055=CARTESIAN_POINT('',(0.0059658150773882,0.00267516180332607,0.050200895697937));
#20056=CARTESIAN_POINT('',(0.00622663675302494,0.00199622202754049,0.0501680936432468));
#20057=CARTESIAN_POINT('',(0.00651099344925417,0.000602388530043543,0.05010425681266));
#20058=CARTESIAN_POINT('',(0.00653759021180571,-9.93993057869834E-5,0.0500747914560228));
#20059=CARTESIAN_POINT('',(0.00636330161511123,-0.00150278360205708,0.0500120805120238));
#20060=CARTESIAN_POINT('',(0.00615721630509946,-0.00220068351354411,0.0499792279792733));
#20061=CARTESIAN_POINT('',(0.00553676033670485,-0.00347830497921899,0.0499156921049825));
#20062=CARTESIAN_POINT('',(0.00513232728730257,-0.00405110020501809,0.0498863749004916));
#20063=CARTESIAN_POINT('',(0.0041387911019502,-0.00506187756366211,0.049823241605466));
#20064=CARTESIAN_POINT('',(0.00355057709646319,-0.00549052166700355,0.0497903710217429));
#20065=CARTESIAN_POINT('',(0.00228372268767734,-0.00612674763472041,0.0497271942213094));
#20066=CARTESIAN_POINT('',(0.00161460618063539,-0.00633617958351373,0.0496978848300432));
#20067=CARTESIAN_POINT('',(0.000208606071525814,-0.0065353353655344,0.0496343860591597));
#20068=CARTESIAN_POINT('',(-0.000518900078309723,-0.00651774283233561,0.0496015299121185));
#20069=CARTESIAN_POINT('',(-0.00190855809191155,-0.00625360975193776,0.0495387691945051));
#20070=CARTESIAN_POINT('',(-0.00256826845705628,-0.00601329722457722,0.0495093272538655));
#20071=CARTESIAN_POINT('',(-0.00380776289581589,-0.00531570203339748,0.0494455210097757));
#20072=CARTESIAN_POINT('',(-0.00437421795963069,-0.0048594189913196,0.049412711738628));
#20073=CARTESIAN_POINT('',(-0.00531494605788761,-0.0038077662865909,0.0493504228378307));
#20074=CARTESIAN_POINT('',(-0.00569422021225458,-0.00321448480076881,0.0493207083866951));
#20075=CARTESIAN_POINT('',(-0.00625510978961098,-0.00190542852921204,0.0492566536267806));
#20076=CARTESIAN_POINT('',(-0.00642702787888753,-0.00119927714474249,0.0492239235136309));
#20077=CARTESIAN_POINT('',(-0.0065347900081369,0.000203648165848476,0.0491621607304204));
#20078=CARTESIAN_POINT('',(-0.00647555925786837,0.00090839605602264,0.0491320346317823));
#20079=CARTESIAN_POINT('',(-0.00594944360627666,0.00298099398905514,0.049035669317932));
#20080=CARTESIAN_POINT('',(-0.00514941531216868,0.00421526192212428,0.0489754985627794));
#20081=CARTESIAN_POINT('',(-0.00291101632274778,0.00598422050880514,0.048846754562263));
#20082=CARTESIAN_POINT('',(-0.00152663083830425,0.00647732477884384,0.0487867687682968));
#20083=CARTESIAN_POINT('',(0.00132703907897548,0.00652114294353052,0.0486578893101228));
#20084=CARTESIAN_POINT('',(0.00272549909433502,0.00607109015430752,0.0485979737679985));
#20085=CARTESIAN_POINT('',(0.00501803035286572,0.0043710241766283,0.048469080736597));
#20086=CARTESIAN_POINT('',(0.00585487210850577,0.00316319651939615,0.0484091205156593));
#20087=CARTESIAN_POINT('',(0.00664142800919386,0.00042044455755067,0.0482803358382475));
#20088=CARTESIAN_POINT('',(0.00657143556203462,-0.00104840443285802,0.0482202161486085));
#20089=CARTESIAN_POINT('',(0.00578979634639851,-0.00303915902305769,0.0481238000953949));
#20090=CARTESIAN_POINT('',(0.00542633082347876,-0.00364681078028188,0.0480935635664421));
#20091=CARTESIAN_POINT('',(0.00474737139188325,-0.00445376679180473,0.0480473347232857));
#20092=CARTESIAN_POINT('',(0.00449681825450261,-0.00470696398512329,0.0480314587978482));
#20093=CARTESIAN_POINT('',(0.00395553899020957,-0.00517016398852178,0.0479993857674241));
#20094=CARTESIAN_POINT('',(0.00366004488627924,-0.00537184808729585,0.0479832352812528));
#20095=CARTESIAN_POINT('',(0.00336685009946227,-0.00557505095485768,0.0479671284889492));
#20096=CARTESIAN_POINT('',(-0.00682733698154762,0.,0.0507966910355878));
#20097=CARTESIAN_POINT('',(-0.00682733698154762,0.00146227267850127,0.0507368944104981));
#20098=CARTESIAN_POINT('',(-0.0063148651064283,0.00298148932551787,0.0506688627636233));
#20099=CARTESIAN_POINT('',(-0.00497745645513572,0.00473033031717387,0.0505781413353049));
#20100=CARTESIAN_POINT('',(-0.00442440985177819,0.00525342227039878,0.0505456830509742));
#20101=CARTESIAN_POINT('',(-0.00317984819977019,0.00608789072783439,0.0504813005051662));
#20102=CARTESIAN_POINT('',(-0.00249865565386296,0.00639621243935651,0.0504505552509165));
#20103=CARTESIAN_POINT('',(-0.00107725861010421,0.00678191179041106,0.0503894389036528));
#20104=CARTESIAN_POINT('',(-0.000318965846980269,0.00686086011488066,0.0503568343023965));
#20105=CARTESIAN_POINT('',(0.00117556315177092,0.0067669189446674,0.0502925734727539));
#20106=CARTESIAN_POINT('',(0.00189966979862991,0.00659920323734378,0.0502623930119793));
#20107=CARTESIAN_POINT('',(0.00326724038291374,0.00604014643794775,0.0502006920662544));
#20108=CARTESIAN_POINT('',(0.00391791592174717,0.00564110069240482,0.0501679727475682));
#20109=CARTESIAN_POINT('',(0.00504643090089172,0.00465892877754698,0.0501038940133495));
#20110=CARTESIAN_POINT('',(0.00551772662206526,0.00408852377527819,0.0500741406143251));
#20111=CARTESIAN_POINT('',(0.00626625075429644,0.00280988170945719,0.0500119076035247));
#20112=CARTESIAN_POINT('',(0.00654020728839858,0.00209675084184725,0.0499791055488345));
#20113=CARTESIAN_POINT('',(0.00683888405580113,0.000632724536680984,0.0499152687182477));
#20114=CARTESIAN_POINT('',(0.00686682021896383,-0.000104405008667636,0.0498858033616105));
#20115=CARTESIAN_POINT('',(0.00668375452947548,-0.0015784630863981,0.0498230924176116));
#20116=CARTESIAN_POINT('',(0.00646729085895286,-0.00231150891333874,0.049790239884861));
#20117=CARTESIAN_POINT('',(0.00581558901611555,-0.00365347080272662,0.0497267040105703));
#20118=CARTESIAN_POINT('',(0.00539078890615489,-0.00425511173010386,0.0496973868060793));
#20119=CARTESIAN_POINT('',(0.00434721869988382,-0.00531679136714716,0.0496342535110538));
#20120=CARTESIAN_POINT('',(0.00372938251023371,-0.00576702178848028,0.0496013829273307));
#20121=CARTESIAN_POINT('',(0.00239872990171982,-0.00643528780048248,0.0495382061268972));
#20122=CARTESIAN_POINT('',(0.00169591699810574,-0.00665526664496158,0.049508896735631));
#20123=CARTESIAN_POINT('',(0.000219111376415932,-0.00686445181968139,0.0494453979647474));
#20124=CARTESIAN_POINT('',(-0.000545031645287988,-0.00684597333468028,0.0494125418177063));
#20125=CARTESIAN_POINT('',(-0.00200467219112918,-0.006568538635011,0.0493497811000929));
#20126=CARTESIAN_POINT('',(-0.00269760526390808,-0.00631612408036826,0.0493203391594533));
#20127=CARTESIAN_POINT('',(-0.00399952006701057,-0.00558339831930807,0.0492565329153635));
#20128=CARTESIAN_POINT('',(-0.00459450154479021,-0.00510413707511864,0.0492237236442158));
#20129=CARTESIAN_POINT('',(-0.00558260427322259,-0.00399952362854343,0.0491614347434185));
#20130=CARTESIAN_POINT('',(-0.00598097849787717,-0.00337636476260179,0.0491317202922829));
#20131=CARTESIAN_POINT('',(-0.00657011421388486,-0.00200138502510542,0.0490676655323683));
#20132=CARTESIAN_POINT('',(-0.00675069001830252,-0.00125967218483466,0.0490349354192187));
#20133=CARTESIAN_POINT('',(-0.0068638789983386,0.000213903792911022,0.0489731726360082));
#20134=CARTESIAN_POINT('',(-0.00680166541499197,0.000954142459565442,0.04894304653737));
#20135=CARTESIAN_POINT('',(-0.00624905482350225,0.00313111546203805,0.0488466812235198));
#20136=CARTESIAN_POINT('',(-0.00540873747601797,0.00442754055505055,0.0487865104683671));
#20137=CARTESIAN_POINT('',(-0.00305761375295149,0.00628558307469247,0.0486577664678508));
#20138=CARTESIAN_POINT('',(-0.00160351125838856,0.00680351984678389,0.0485977806738846));
#20139=CARTESIAN_POINT('',(0.00139386815074587,0.00684954467389603,0.0484689012157106));
#20140=CARTESIAN_POINT('',(0.00286275396306585,0.00637682743520206,0.0484089856735863));
#20141=CARTESIAN_POINT('',(0.00527073603117671,0.00459114692435894,0.0482800926421847));
#20142=CARTESIAN_POINT('',(0.00614972074902048,0.00332249362719632,0.048220132421247));
#20143=CARTESIAN_POINT('',(0.00697588723960853,0.000441617950224018,0.0480913477438352));
#20144=CARTESIAN_POINT('',(0.00690237000531325,-0.00110120159324154,0.0480312280541963));
#20145=CARTESIAN_POINT('',(0.0060813678017532,-0.00319220966014245,0.0479348120009826));
#20146=CARTESIAN_POINT('',(0.00569959832388436,-0.00383046247768077,0.0479045754720299));
#20147=CARTESIAN_POINT('',(0.00498644681060703,-0.00467805641921186,0.0478583466288735));
#20148=CARTESIAN_POINT('',(0.00472327593357909,-0.00494400450560692,0.047842470703436));
#20149=CARTESIAN_POINT('',(0.00415473809689405,-0.005430531046077,0.0478103976730118));
#20150=CARTESIAN_POINT('',(0.00384436304711054,-0.00564237186240781,0.0477942471868405));
#20151=CARTESIAN_POINT('',(0.00353640310698247,-0.00585580793201727,0.047778140394537));
#20152=CARTESIAN_POINT('',(-0.00715467396309524,0.,0.0506077029411755));
#20153=CARTESIAN_POINT('',(-0.00715467396309523,0.00153238140846052,0.0505479063160859));
#20154=CARTESIAN_POINT('',(-0.00661763160065663,0.00312443696659216,0.0504798746692111));
#20155=CARTESIAN_POINT('',(-0.00521610083085826,0.00495712621899208,0.0503891532408927));
#20156=CARTESIAN_POINT('',(-0.00463653838299393,0.0055052978396632,0.050356694956562));
#20157=CARTESIAN_POINT('',(-0.00333230616607618,0.0063797749251762,0.0502923124107539));
#20158=CARTESIAN_POINT('',(-0.00261845381262866,0.00670287913515533,0.0502615671565042));
#20159=CARTESIAN_POINT('',(-0.00112890782307418,0.0071070708591073,0.0502004508092405));
#20160=CARTESIAN_POINT('',(-0.000334258678995079,0.00718980436457791,0.0501678462079842));
#20161=CARTESIAN_POINT('',(0.00123192558045422,0.00709135918069376,0.0501035853783417));
#20162=CARTESIAN_POINT('',(0.00199074955337196,0.00691560233616806,0.050073404917567));
#20163=CARTESIAN_POINT('',(0.00342388837140823,0.0063297415331433,0.0500117039718421));
#20164=CARTESIAN_POINT('',(0.00410576057849229,0.00591156352121328,0.049978984653156));
#20165=CARTESIAN_POINT('',(0.00528838225954753,0.00488230132930608,0.0499149059189373));
#20166=CARTESIAN_POINT('',(0.00578227427547,0.00428454823330661,0.0498851525199129));
#20167=CARTESIAN_POINT('',(0.00656668643120468,0.0029446016155883,0.0498229195091125));
#20168=CARTESIAN_POINT('',(0.00685377782377222,0.00219727965615402,0.0497901174544223));
#20169=CARTESIAN_POINT('',(0.00716677466234808,0.000663060543318424,0.0497262806238355));
#20170=CARTESIAN_POINT('',(0.00719605022612195,-0.000109410711548288,0.0496968152671983));
#20171=CARTESIAN_POINT('',(0.00700420744383973,-0.00165414257073912,0.0496341043231993));
#20172=CARTESIAN_POINT('',(0.00677736541280625,-0.00242233431313338,0.0496012517904488));
#20173=CARTESIAN_POINT('',(0.00609441769552624,-0.00382863662623425,0.049537715916158));
#20174=CARTESIAN_POINT('',(0.00564925052500722,-0.00445912325518964,0.0495083987116671));
#20175=CARTESIAN_POINT('',(0.00455564629781744,-0.0055717051706322,0.0494452654166416));
#20176=CARTESIAN_POINT('',(0.00390818792400423,-0.00604352190995701,0.0494123948329184));
#20177=CARTESIAN_POINT('',(0.0025137371157623,-0.00674382796624454,0.0493492180324849));
#20178=CARTESIAN_POINT('',(0.0017772278155761,-0.00697435370640943,0.0493199086412188));
#20179=CARTESIAN_POINT('',(0.00022961668130605,-0.00719356827382838,0.0492564098703352));
#20180=CARTESIAN_POINT('',(-0.000571163212266254,-0.00717420383702495,0.049223553723294));
#20181=CARTESIAN_POINT('',(-0.00210078629034681,-0.00688346751808424,0.0491607930056807));
#20182=CARTESIAN_POINT('',(-0.00282694207075989,-0.0066189509361593,0.049131351065041));
#20183=CARTESIAN_POINT('',(-0.00419127723820524,-0.00585109460521867,0.0490675448209512));
#20184=CARTESIAN_POINT('',(-0.00481478512994973,-0.00534885515891767,0.0490347355498035));
#20185=CARTESIAN_POINT('',(-0.00585026248855756,-0.00419128097049597,0.0489724466490063));
#20186=CARTESIAN_POINT('',(-0.00626773678349976,-0.00353824472443477,0.0489427321978707));
#20187=CARTESIAN_POINT('',(-0.00688511863815874,-0.00209734152099881,0.0488786774379561));
#20188=CARTESIAN_POINT('',(-0.00707435215771751,-0.00132006722492682,0.0488459473248065));
#20189=CARTESIAN_POINT('',(-0.00719296798854031,0.000224159419973568,0.048784184541596));
#20190=CARTESIAN_POINT('',(-0.00712777157211556,0.000999888863108244,0.0487540584429578));
#20191=CARTESIAN_POINT('',(-0.00654866604072785,0.00328123693502096,0.0486576931291076));
#20192=CARTESIAN_POINT('',(-0.00566805963986726,0.00463981918797682,0.0485975223739549));
#20193=CARTESIAN_POINT('',(-0.0032042111831552,0.0065869456405798,0.0484687783734385));
#20194=CARTESIAN_POINT('',(-0.00168039167847287,0.00712971491472395,0.0484087925794723));
#20195=CARTESIAN_POINT('',(0.00146069722251627,0.00717794640426154,0.0482799131212984));
#20196=CARTESIAN_POINT('',(0.00300000883179668,0.0066825647160966,0.0482199975791741));
#20197=CARTESIAN_POINT('',(0.00552344170948769,0.00481126967208959,0.0480911045477725));
#20198=CARTESIAN_POINT('',(0.0064445693895352,0.00348179073499648,0.0480311443268348));
#20199=CARTESIAN_POINT('',(0.0073103464700232,0.000462791342897367,0.047902359649423));
#20200=CARTESIAN_POINT('',(0.00723330444859188,-0.00115399875362506,0.0478422399597841));
#20201=CARTESIAN_POINT('',(0.0063729392571079,-0.0033452602972272,0.0477458239065704));
#20202=CARTESIAN_POINT('',(0.00597286582428995,-0.00401411417507966,0.0477155873776177));
#20203=CARTESIAN_POINT('',(0.00522552222933081,-0.004902346046619,0.0476693585344612));
#20204=CARTESIAN_POINT('',(0.00494973361265557,-0.00518104502609055,0.0476534826090237));
#20205=CARTESIAN_POINT('',(0.00435393720357852,-0.00569089810363222,0.0476214095785996));
#20206=CARTESIAN_POINT('',(0.00402868120794183,-0.00591289563751978,0.0476052590924282));
#20207=CARTESIAN_POINT('',(0.00370595611450266,-0.00613656490917685,0.0475891523001247));
#20208=CARTESIAN_POINT('',(-0.00748201094464286,0.,0.0504187148467633));
#20209=CARTESIAN_POINT('',(-0.00748201094464285,0.00160249013841978,0.0503589182216737));
#20210=CARTESIAN_POINT('',(-0.00692039809488496,0.00326738460766644,0.0502908865747988));
#20211=CARTESIAN_POINT('',(-0.00545474520658079,0.00518392212081029,0.0502001651464805));
#20212=CARTESIAN_POINT('',(-0.00484866691420967,0.00575717340892763,0.0501677068621498));
#20213=CARTESIAN_POINT('',(-0.00348476413238216,0.00667165912251801,0.0501033243163417));
#20214=CARTESIAN_POINT('',(-0.00273825197139437,0.00700954583095415,0.050072579062092));
#20215=CARTESIAN_POINT('',(-0.00118055703604415,0.00743222992780353,0.0500114627148283));
#20216=CARTESIAN_POINT('',(-0.000349551511009888,0.00751874861427516,0.049978858113572));
#20217=CARTESIAN_POINT('',(0.00128828800913751,0.00741579941672012,0.0499145972839295));
#20218=CARTESIAN_POINT('',(0.00208182930811401,0.00723200143499235,0.0498844168231548));
#20219=CARTESIAN_POINT('',(0.00358053635990272,0.00661933662833886,0.0498227158774299));
#20220=CARTESIAN_POINT('',(0.00429360523523741,0.00618202635002174,0.0497899965587437));
#20221=CARTESIAN_POINT('',(0.00553033361820334,0.00510567388106518,0.049725917824525));
#20222=CARTESIAN_POINT('',(0.00604682192887473,0.00448057269133503,0.0496961644255007));
#20223=CARTESIAN_POINT('',(0.00686712210811291,0.00307932152171942,0.0496339314147002));
#20224=CARTESIAN_POINT('',(0.00716734835914586,0.00229780847046079,0.04960112936001));
#20225=CARTESIAN_POINT('',(0.00749466526889503,0.000693396549955864,0.0495372925294232));
#20226=CARTESIAN_POINT('',(0.00752528023328007,-0.00011441641442894,0.049507827172786));
#20227=CARTESIAN_POINT('',(0.00732466035820398,-0.00172982205508014,0.0494451162287871));
#20228=CARTESIAN_POINT('',(0.00708743996665964,-0.00253315971292801,0.0494122636960365));
#20229=CARTESIAN_POINT('',(0.00637324637493694,-0.00400380244974188,0.0493487278217458));
#20230=CARTESIAN_POINT('',(0.00590771214385954,-0.00466313478027542,0.0493194106172549));
#20231=CARTESIAN_POINT('',(0.00476407389575106,-0.00582661897411724,0.0492562773222293));
#20232=CARTESIAN_POINT('',(0.00408699333777475,-0.00632002203143374,0.0492234067385062));
#20233=CARTESIAN_POINT('',(0.00262874432980478,-0.0070523681320066,0.0491602299380727));
#20234=CARTESIAN_POINT('',(0.00185853863304645,-0.00729344076785728,0.0491309205468065));
#20235=CARTESIAN_POINT('',(0.000240121986196168,-0.00752268472797537,0.049067421775923));
#20236=CARTESIAN_POINT('',(-0.000597294779244519,-0.00750243433936963,0.0490345656288818));
#20237=CARTESIAN_POINT('',(-0.00219690038956444,-0.00719839640115748,0.0489718049112684));
#20238=CARTESIAN_POINT('',(-0.0029562788776117,-0.00692177779195035,0.0489423629706288));
#20239=CARTESIAN_POINT('',(-0.00438303440939992,-0.00611879089112926,0.048878556726539));
#20240=CARTESIAN_POINT('',(-0.00503506871510925,-0.00559357324271671,0.0488457474553913));
#20241=CARTESIAN_POINT('',(-0.00611792070389254,-0.0043830383124485,0.048783458554594));
#20242=CARTESIAN_POINT('',(-0.00655449506912235,-0.00370012468626775,0.0487537441034584));
#20243=CARTESIAN_POINT('',(-0.00720012306243262,-0.00219329801689219,0.0486896893435438));
#20244=CARTESIAN_POINT('',(-0.0073980142971325,-0.00138046226501898,0.0486569592303942));
#20245=CARTESIAN_POINT('',(-0.00752205697874201,0.000234415047036114,0.0485951964471837));
#20246=CARTESIAN_POINT('',(-0.00745387772923916,0.00104563526665105,0.0485650703485456));
#20247=CARTESIAN_POINT('',(-0.00684827725795344,0.00343135840800387,0.0484687050346953));
#20248=CARTESIAN_POINT('',(-0.00592738180371655,0.0048520978209031,0.0484085342795426));
#20249=CARTESIAN_POINT('',(-0.00335080861335891,0.00688830820646713,0.0482797902790263));
#20250=CARTESIAN_POINT('',(-0.00175727209855718,0.007455909982664,0.0482198044850601));
#20251=CARTESIAN_POINT('',(0.00152752629428666,0.00750634813462706,0.0480909250268861));
#20252=CARTESIAN_POINT('',(0.00313726370052751,0.00698830199699114,0.0480310094847618));
#20253=CARTESIAN_POINT('',(0.00577614738779868,0.00503139241982023,0.0479021164533603));
#20254=CARTESIAN_POINT('',(0.00673941803004991,0.00364108784279665,0.0478421562324226));
#20255=CARTESIAN_POINT('',(0.00764480570043787,0.000483964735570715,0.0477133715550107));
#20256=CARTESIAN_POINT('',(0.00756423889187051,-0.00120679591400858,0.0476532518653718));
#20257=CARTESIAN_POINT('',(0.0066645107124626,-0.00349831093431196,0.0475568358121581));
#20258=CARTESIAN_POINT('',(0.00624613332469554,-0.00419776587247855,0.0475265992832054));
#20259=CARTESIAN_POINT('',(0.00546459764805459,-0.00512663567402613,0.047480370440049));
#20260=CARTESIAN_POINT('',(0.00517619129173205,-0.00541808554657418,0.0474644945146114));
#20261=CARTESIAN_POINT('',(0.004553136310263,-0.00595126516118744,0.0474324214841873));
#20262=CARTESIAN_POINT('',(0.00421299936877313,-0.00618341941263174,0.047416270998016));
#20263=CARTESIAN_POINT('',(0.00387550912202286,-0.00641732188633643,0.0474001642057124));
#20264=CARTESIAN_POINT('',(-0.00699100547232143,0.,0.0507021969883817));
#20265=CARTESIAN_POINT('',(-0.0065,0.,0.05098567913));
#20266=CARTESIAN_POINT('',(-0.00748201094464286,0.,0.0504187148467633));
#20267=CARTESIAN_POINT('',(-0.0065,0.,0.05098567913));
#20268=CARTESIAN_POINT('',(-0.0065,0.00211197802551389,0.0508949648442857));
#20269=CARTESIAN_POINT('',(-0.00525861046343716,0.00382060413990108,0.0508042505585714));
#20270=CARTESIAN_POINT('',(-0.00401722092687431,0.00552923025428826,0.0507135362728571));
#20271=CARTESIAN_POINT('',(-0.00200861046343716,0.0061818673559185,0.0506228219871429));
#20272=CARTESIAN_POINT('',(5.7699056946876E-18,0.00683450445754873,0.0505321077014286));
#20273=CARTESIAN_POINT('',(0.00200861046343717,0.0061818673559185,0.0504413934157143));
#20274=CARTESIAN_POINT('',(0.00401722092687432,0.00552923025428826,0.05035067913));
#20275=CARTESIAN_POINT('',(0.00525861046343717,0.00382060413990108,0.0502599648442857));
#20276=CARTESIAN_POINT('',(0.0065,0.00211197802551392,0.0501692505585715));
#20277=CARTESIAN_POINT('',(0.0065,7.9602041944578E-19,0.0500785362728571));
#20278=CARTESIAN_POINT('',(0.0065,7.9602041944578E-19,0.0500785362728572));
#20279=CARTESIAN_POINT('',(0.0065,7.96020419445781E-19,0.0500785362728572));
#20280=CARTESIAN_POINT('',(0.00650000000000003,-0.00211197802551387,0.0499878219871428));
#20281=CARTESIAN_POINT('',(0.00525861046343717,-0.00382060413990108,0.0498971077014286));
#20282=CARTESIAN_POINT('',(0.00401722092687432,-0.00552923025428826,0.0498063934157143));
#20283=CARTESIAN_POINT('',(0.00200861046343717,-0.0061818673559185,0.04971567913));
#20284=CARTESIAN_POINT('',(7.33278353658974E-18,-0.00683450445754873,0.0496249648442857));
#20285=CARTESIAN_POINT('',(-0.00200861046343716,-0.0061818673559185,0.0495342505585714));
#20286=CARTESIAN_POINT('',(-0.00401722092687431,-0.00552923025428826,0.0494435362728571));
#20287=CARTESIAN_POINT('',(-0.00525861046343716,-0.00382060413990108,0.0493528219871429));
#20288=CARTESIAN_POINT('',(-0.00649999999999999,-0.00211197802551391,0.0492621077014285));
#20289=CARTESIAN_POINT('',(-0.0065,0.,0.0491713934157143));
#20290=CARTESIAN_POINT('',(-0.0065,0.,0.0491713934157143));
#20291=CARTESIAN_POINT('',(-0.0065,0.,0.0491713934157143));
#20292=CARTESIAN_POINT('',(-0.00650000000000001,0.00211197802551388,0.04908067913));
#20293=CARTESIAN_POINT('',(-0.00525861046343716,0.00382060413990108,0.0489899648442857));
#20294=CARTESIAN_POINT('',(-0.00401722092687431,0.00552923025428826,0.0488992505585714));
#20295=CARTESIAN_POINT('',(-0.00200861046343716,0.0061818673559185,0.0488085362728572));
#20296=CARTESIAN_POINT('',(5.54771977541372E-18,0.00683450445754873,0.0487178219871428));
#20297=CARTESIAN_POINT('',(0.00200861046343717,0.0061818673559185,0.0486271077014286));
#20298=CARTESIAN_POINT('',(0.00401722092687432,0.00552923025428826,0.0485363934157143));
#20299=CARTESIAN_POINT('',(0.00525861046343717,0.00382060413990108,0.04844567913));
#20300=CARTESIAN_POINT('',(0.00649999999999998,0.00211197802551393,0.0483549648442856));
#20301=CARTESIAN_POINT('',(0.0065,7.96020419445779E-19,0.0482642505585714));
#20302=CARTESIAN_POINT('',(0.0065,7.9602041944578E-19,0.0482642505585714));
#20303=CARTESIAN_POINT('',(0.0065,7.96020419445781E-19,0.0482642505585715));
#20304=CARTESIAN_POINT('',(0.00650000000000004,-0.00211197802551386,0.0481735362728571));
#20305=CARTESIAN_POINT('',(0.00525861046343717,-0.00382060413990108,0.0480828219871429));
#20306=CARTESIAN_POINT('',(0.00460981098571225,-0.0047136000110528,0.0480354110984088));
#20307=CARTESIAN_POINT('',(0.00370259321821895,-0.00534235935335683,0.0479855726937042));
#20308=CARTESIAN_POINT('',(0.00370259421038123,-0.00534235866572474,0.0479855727658843));
#20309=CARTESIAN_POINT('',(0.00398228679950131,-0.00574591588526488,0.047702090660359));
#20310=CARTESIAN_POINT('',(0.00426198038078367,-0.00614947241717293,0.0474186086270138));
#20311=CARTESIAN_POINT('',(-0.00748201094464286,0.,0.0504187148467633));
#20312=CARTESIAN_POINT('',(-0.00748201094464285,0.00243105272334464,0.050328000561049));
#20313=CARTESIAN_POINT('',(-0.00605307400631542,0.00439781569075195,0.0502372862753347));
#20314=CARTESIAN_POINT('',(-0.00462413706798799,0.00636457865815926,0.0501465719896204));
#20315=CARTESIAN_POINT('',(-0.00231206853399399,0.00711581526389425,0.0500558577039062));
#20316=CARTESIAN_POINT('',(5.63724730105931E-18,0.00786705186962924,0.0499651434181919));
#20317=CARTESIAN_POINT('',(0.00231206853399401,0.00711581526389425,0.0498744291324776));
#20318=CARTESIAN_POINT('',(0.004624137067988,0.00636457865815926,0.0497837148467633));
#20319=CARTESIAN_POINT('',(0.00605307400631544,0.00439781569075195,0.049693000561049));
#20320=CARTESIAN_POINT('',(0.00748201094464287,0.00243105272334464,0.0496022862753347));
#20321=CARTESIAN_POINT('',(0.00748201094464287,9.16282075454235E-19,0.0495115719896204));
#20322=CARTESIAN_POINT('',(0.00748201094464287,-0.00243105272334463,0.0494208577039061));
#20323=CARTESIAN_POINT('',(0.00605307400631544,-0.00439781569075195,0.0493301434181919));
#20324=CARTESIAN_POINT('',(0.004624137067988,-0.00636457865815926,0.0492394291324775));
#20325=CARTESIAN_POINT('',(0.00231206853399401,-0.00711581526389425,0.0491487148467633));
#20326=CARTESIAN_POINT('',(7.45302631959591E-18,-0.00786705186962924,0.049058000561049));
#20327=CARTESIAN_POINT('',(-0.00231206853399399,-0.00711581526389425,0.0489672862753347));
#20328=CARTESIAN_POINT('',(-0.00462413706798798,-0.00636457865815926,0.0488765719896204));
#20329=CARTESIAN_POINT('',(-0.00605307400631542,-0.00439781569075195,0.0487858577039062));
#20330=CARTESIAN_POINT('',(-0.00748201094464285,-0.00243105272334464,0.0486951434181918));
#20331=CARTESIAN_POINT('',(-0.00748201094464286,0.,0.0486044291324776));
#20332=CARTESIAN_POINT('',(-0.00748201094464285,0.00243105272334464,0.0485137148467633));
#20333=CARTESIAN_POINT('',(-0.00605307400631542,0.00439781569075195,0.048423000561049));
#20334=CARTESIAN_POINT('',(-0.00462413706798799,0.00636457865815926,0.0483322862753347));
#20335=CARTESIAN_POINT('',(-0.00231206853399399,0.00711581526389425,0.0482415719896204));
#20336=CARTESIAN_POINT('',(5.41506138178544E-18,0.00786705186962924,0.0481508577039061));
#20337=CARTESIAN_POINT('',(0.00231206853399401,0.00711581526389425,0.0480601434181919));
#20338=CARTESIAN_POINT('',(0.004624137067988,0.00636457865815926,0.0479694291324776));
#20339=CARTESIAN_POINT('',(0.00605307400631544,0.00439781569075195,0.0478787148467633));
#20340=CARTESIAN_POINT('',(0.00748201094464287,0.00243105272334464,0.047788000561049));
#20341=CARTESIAN_POINT('',(0.00748201094464287,9.16282075454235E-19,0.0476972862753347));
#20342=CARTESIAN_POINT('',(0.00748201094464287,-0.00243105272334463,0.0476065719896204));
#20343=CARTESIAN_POINT('',(0.00605307400631544,-0.00439781569075195,0.0475158577039062));
#20344=CARTESIAN_POINT('',(0.00530625647659887,-0.00542572183654477,0.0474684469211417));
#20345=CARTESIAN_POINT('',(0.00426198038078368,-0.00614947241717293,0.0474186086270138));
#20346=CARTESIAN_POINT('',(1.0842021724855E-17,1.47451495458029E-17,0.0497741129358333));
#20347=CARTESIAN_POINT('',(-0.00748201094464286,0.,0.0503053219896204));
#20348=CARTESIAN_POINT('',(0.004261979825191,-0.00614947280223435,0.0473052157433551));
#20349=CARTESIAN_POINT('',(0.00426197926959833,-0.00614947318729578,0.0472485192882679));
#20350=CARTESIAN_POINT('',(0.00370259619470581,-0.00534235729046056,0.0472485192882679));
#20351=CARTESIAN_POINT('',(0.00370259619470735,-0.00534235729045949,0.04678567913));
#20352=CARTESIAN_POINT('',(0.00353170713956903,-0.00509578695397652,0.04678567913));
#20353=CARTESIAN_POINT('',(-0.00748201094464286,0.,0.0503053219896204));
#20354=CARTESIAN_POINT('',(-0.0065,0.,0.0503053219896204));
#20355=CARTESIAN_POINT('',(0.0083,0.,0.00847567913));
#20356=CARTESIAN_POINT('',(1.03797133171545E-18,0.,0.00847567913));
#20357=CARTESIAN_POINT('',(-0.0084,0.,0.00847567913));
#20358=CARTESIAN_POINT('',(1.03797133171545E-18,0.,0.00847567913));
#20359=CARTESIAN_POINT('',(-0.0096,0.,0.00847567913));
#20360=CARTESIAN_POINT('',(0.0099,0.,0.01077567913));
#20361=CARTESIAN_POINT('',(1.31964009551934E-18,0.,0.01077567913));
#20362=CARTESIAN_POINT('',(0.0084,0.,0.01077567913));
#20363=CARTESIAN_POINT('',(1.31964009551934E-18,0.,0.01077567913));
#20364=CARTESIAN_POINT('',(0.0096,0.,0.01077567913));
#20365=CARTESIAN_POINT('',(0.0099,0.,0.01962567913));
#20366=CARTESIAN_POINT('',(2.40345251276475E-18,0.,0.01962567913));
#20367=CARTESIAN_POINT('',(-0.0075,0.,0.01962567913));
#20368=CARTESIAN_POINT('',(2.40345251276475E-18,0.,0.01962567913));
#20369=CARTESIAN_POINT('',(-0.0099,0.,0.01962567913));
#20370=CARTESIAN_POINT('',(0.0065,0.,0.04648567913));
#20371=CARTESIAN_POINT('',(5.69285381527454E-18,0.,0.04648567913));
#20372=CARTESIAN_POINT('',(0.00550000000000001,0.,0.04648567913));
#20373=CARTESIAN_POINT('',(5.69285381527454E-18,0.,0.04648567913));
#20374=CARTESIAN_POINT('',(0.00620000000000001,0.,0.04648567913));
#20375=CARTESIAN_POINT('',(0.0045,0.,0.05148567913));
#20376=CARTESIAN_POINT('',(6.30517721484821E-18,0.,0.05148567913));
#20377=CARTESIAN_POINT('',(-0.00549999999999999,0.,0.05148567913));
#20378=CARTESIAN_POINT('',(6.30517721484821E-18,0.,0.05148567913));
#20379=CARTESIAN_POINT('',(-0.00619999999999999,0.,0.05148567913));
#20380=CARTESIAN_POINT('',(0.00261523063261998,0.,0.06962567913));
#20381=CARTESIAN_POINT('',(8.52668650850151E-18,0.,0.06962567913));
#20382=CARTESIAN_POINT('',(-0.00261523063261996,0.,0.06962567913));
#20383=CARTESIAN_POINT('',(8.52668650850151E-18,0.,0.06962567913));
#20384=CARTESIAN_POINT('',(-0.00449999999999999,0.,0.06962567913));
#20385=CARTESIAN_POINT('',(0.00075,0.,0.06462567913));
#20386=CARTESIAN_POINT('',(7.91436310892783E-18,0.,0.06462567913));
#20387=CARTESIAN_POINT('',(0.000950000000000008,0.,0.06462567913));
#20388=CARTESIAN_POINT('',(7.91436310892783E-18,0.,0.06462567913));
#20389=CARTESIAN_POINT('',(0.00280000000000001,0.,0.06462567913));
#20390=CARTESIAN_POINT('',(0.0065,0.,0.01762567913));
#20391=CARTESIAN_POINT('',(2.15852315293528E-18,0.,0.01762567913));
#20392=CARTESIAN_POINT('',(-0.0075,0.,0.01762567913));
#20393=CARTESIAN_POINT('',(2.15852315293528E-18,0.,0.01762567913));
#20394=CARTESIAN_POINT('',(-0.004,0.,0.01762567913));
#20395=CARTESIAN_POINT('',(0.0075,0.,-0.00037432087));
#20396=CARTESIAN_POINT('',(-4.58410855299551E-20,0.,-0.000374320869999999));
#20397=CARTESIAN_POINT('',(-0.0099,0.,-0.000374320869999998));
#20398=CARTESIAN_POINT('',(-4.58410855299551E-20,0.,-0.000374320869999999));
#20399=CARTESIAN_POINT('',(0.008,0.,-0.00037432087));
#20400=CARTESIAN_POINT('',(0.,0.,0.));
#20401=CARTESIAN_POINT('',(6.42764189476295E-18,0.,0.05248567913));
#20402=CARTESIAN_POINT('',(-0.00449999999999999,0.,0.05248567913));
#20403=CARTESIAN_POINT('',(0.,0.,0.));
#20404=CARTESIAN_POINT('',(5.72959321924896E-18,0.,0.04678567913));
#20405=CARTESIAN_POINT('',(6.26843781087379E-18,0.,0.05118567913));
#20406=CARTESIAN_POINT('',(-0.00649999999999999,0.,0.05118567913));
#20407=CARTESIAN_POINT('',(0.,0.,0.));
#20408=CARTESIAN_POINT('',(1.53912544274125E-20,0.,0.000125679130000001));
#20409=CARTESIAN_POINT('',(0.0075,0.,0.00012567913));
#20410=CARTESIAN_POINT('',(2.60208521396521E-18,0.,0.01862567913));
#20411=CARTESIAN_POINT('',(2.28098783285001E-18,0.,0.01862567913));
#20412=CARTESIAN_POINT('',(-0.003,0.,0.01862567913));
#20413=CARTESIAN_POINT('',(0.,0.,0.));
#20414=CARTESIAN_POINT('',(7.88987017294488E-18,0.,0.06442567913));
#20415=CARTESIAN_POINT('',(0.00300000000000001,0.,0.06442567913));
#20416=CARTESIAN_POINT('',(0.,0.,0.));
#20417=CARTESIAN_POINT('',(7.93885604491078E-18,0.,0.06482567913));
#20418=CARTESIAN_POINT('',(0.000750000000000008,0.,0.06482567913));
#20419=CARTESIAN_POINT('',(8.03682778884257E-18,0.,0.06562567913));
#20420=CARTESIAN_POINT('',(-0.000749999999999992,0.,0.06562567913));
#20421=CARTESIAN_POINT('',(8.03682778884257E-18,0.,0.06562567913));
#20422=CARTESIAN_POINT('',(0.,0.,0.));
#20423=CARTESIAN_POINT('',(0.,0.,0.));
#20424=CARTESIAN_POINT('',(2.77084655250895E-18,0.,0.02262567913));
#20425=CARTESIAN_POINT('',(-0.0045,0.,0.02262567913));
#20426=CARTESIAN_POINT('',(5.5703891353598E-18,0.,0.04548567913));
#20427=CARTESIAN_POINT('',(0.0045,0.,0.04548567913));
#20428=CARTESIAN_POINT('',(2.60208521396521E-18,0.,0.02262567913));
#20429=CARTESIAN_POINT('',(0.,0.,0.));
#20430=CARTESIAN_POINT('',(1.35637949949376E-18,0.,0.01107567913));
#20431=CARTESIAN_POINT('',(0.0099,0.,0.01107567913));
#20432=CARTESIAN_POINT('',(0.,0.,0.));
#20433=CARTESIAN_POINT('',(1.05021779970692E-18,0.,0.00857567913));
#20434=CARTESIAN_POINT('',(-0.0083,0.,0.00857567913));
#20435=CARTESIAN_POINT('',(1.30739362752787E-18,0.,0.01067567913));
#20436=CARTESIAN_POINT('',(0.0083,0.,0.01067567913));
#20437=CARTESIAN_POINT('',(0.,0.,0.));
#20438=CARTESIAN_POINT('',(1.00123192774103E-18,0.,0.00817567913));
#20439=CARTESIAN_POINT('',(-0.0099,0.,0.00817567913));
#20440=CARTESIAN_POINT('',(1.30739362752787E-18,0.,0.01067567913));
#20441=CARTESIAN_POINT('',(1.05021779970692E-18,0.,0.00857567913));
#20442=CARTESIAN_POINT('',(7.88987017294488E-18,0.,0.06442567913));
#20443=CARTESIAN_POINT('',(7.93885604491078E-18,0.,0.06482567913));
#20444=CARTESIAN_POINT('',(5.5703891353598E-18,0.,0.04548567913));
#20445=CARTESIAN_POINT('',(6.42764189476295E-18,0.,0.05248567913));
#20446=CARTESIAN_POINT('',(5.72959321924896E-18,0.,0.04678567913));
#20447=CARTESIAN_POINT('',(6.26843781087379E-18,0.,0.05118567913));
#20448=CARTESIAN_POINT('',(1.00123192774103E-18,0.,0.00817567913));
#20449=CARTESIAN_POINT('',(1.35637949949376E-18,0.,0.01107567913));
#20450=CARTESIAN_POINT('',(1.53912544274125E-20,0.,0.000125679130000001));
#20451=CARTESIAN_POINT('',(8.67361737988404E-18,0.,0.07262567913));
#20452=CARTESIAN_POINT('',(6.46618946264691E-18,0.,0.06732567913));
#20453=CARTESIAN_POINT('',(0.00350000000000001,0.,0.06732567913));
#20454=CARTESIAN_POINT('',(6.13299279589414E-18,0.,0.06652567913));
#20455=CARTESIAN_POINT('',(-0.00349999999999999,0.,0.06652567913));
#20456=CARTESIAN_POINT('',(6.13299279589414E-18,0.,0.06652567913));
#20457=CARTESIAN_POINT('',(6.46618946264691E-18,0.,0.06732567913));
#45463=MECHANICAL_DESIGN_GEOMETRIC_PRESENTATION_REPRESENTATION('',(#13530),#45464);
#45464=(
GEOMETRIC_REPRESENTATION_CONTEXT(3)
GLOBAL_UNCERTAINTY_ASSIGNED_CONTEXT((#45492))
GLOBAL_UNIT_ASSIGNED_CONTEXT((#45522,#45521,#45520))
REPRESENTATION_CONTEXT('MAS-690','TOP_LEVEL_ASSEMBLY_PART')
);
#45466=(
GEOMETRIC_REPRESENTATION_CONTEXT(3)
GLOBAL_UNCERTAINTY_ASSIGNED_CONTEXT((#45494))
GLOBAL_UNIT_ASSIGNED_CONTEXT((#45522,#45521,#45520))
REPRESENTATION_CONTEXT('piston','COMPONENT_PART')
);
#45492=UNCERTAINTY_MEASURE_WITH_UNIT(LENGTH_MEASURE(1.E-8),#45522,
'DISTANCE_ACCURACY_VALUE','Maximum Tolerance applied to model');
#45494=UNCERTAINTY_MEASURE_WITH_UNIT(LENGTH_MEASURE(2.E-5),#45522,
'DISTANCE_ACCURACY_VALUE','Maximum Tolerance applied to model');
#45520=(
NAMED_UNIT(*)
SI_UNIT($,.STERADIAN.)
SOLID_ANGLE_UNIT()
);
#45521=(
NAMED_UNIT(*)
PLANE_ANGLE_UNIT()
SI_UNIT($,.RADIAN.)
);
#45522=(
LENGTH_UNIT()
NAMED_UNIT(*)
SI_UNIT($,.METRE.)
);
#45526=PRODUCT_DEFINITION_SHAPE('','',#45587);
#45587=PRODUCT_DEFINITION('','',#45643,#45615);
#45615=PRODUCT_DEFINITION_CONTEXT('',#45782,'design');
#45643=PRODUCT_DEFINITION_FORMATION_WITH_SPECIFIED_SOURCE('','',#45699,
 .NOT_KNOWN.);
#45699=PRODUCT('piston','piston','piston',(#45755));
#45755=PRODUCT_CONTEXT('',#45782,'mechanical');
#45782=APPLICATION_CONTEXT('managed model based 3d engineering');
ENDSEC;
END-ISO-10303-21;
